ISO-10303-21;
HEADER;
/* Generated by software containing ST-Developer
 * from STEP Tools, Inc. (www.steptools.com) 
 */

FILE_DESCRIPTION(
/* description */ ('Spring compression tester'),
/* implementation_level */ '2;1');

FILE_NAME(
/* name */ 'Flanged lead nut.step',
/* time_stamp */ '2026-10-28T03:24:11-07:00',
/* author */ (''),
/* organization */ (''),
/* preprocessor_version */ 'ST-DEVELOPER v20.2',
/* originating_system */ 'Autodesk Translation Framework v15.17.0.0',
/* authorisation */ '');

FILE_SCHEMA (('AUTOMOTIVE_DESIGN { 1 0 10303 214 3 1 1 }'));
ENDSEC;

DATA;
#10=MECHANICAL_DESIGN_GEOMETRIC_PRESENTATION_REPRESENTATION('',(#1166),#43521);
#11=B_SPLINE_SURFACE_WITH_KNOTS('',3,3,((#31855,#31856,#31857,#31858,#31859,
#31860,#31861,#31862,#31863,#31864,#31865,#31866,#31867,#31868,#31869,#31870,
#31871,#31872,#31873,#31874,#31875,#31876,#31877,#31878,#31879,#31880,#31881,
#31882,#31883,#31884,#31885,#31886,#31887,#31888,#31889,#31890,#31891,#31892,
#31893,#31894,#31895,#31896,#31897,#31898,#31899,#31900,#31901,#31902,#31903,
#31904,#31905,#31906,#31907,#31908,#31909,#31910,#31911,#31912,#31913,#31914,
#31915,#31916,#31917,#31918,#31919,#31920,#31921,#31922,#31923,#31924,#31925,
#31926,#31927,#31928,#31929,#31930,#31931,#31932,#31933,#31934,#31935,#31936,
#31937,#31938,#31939,#31940,#31941,#31942,#31943,#31944,#31945,#31946,#31947,
#31948,#31949,#31950,#31951,#31952,#31953,#31954,#31955,#31956,#31957,#31958,
#31959,#31960,#31961,#31962,#31963,#31964,#31965,#31966,#31967,#31968,#31969),
(#31970,#31971,#31972,#31973,#31974,#31975,#31976,#31977,#31978,#31979,
#31980,#31981,#31982,#31983,#31984,#31985,#31986,#31987,#31988,#31989,#31990,
#31991,#31992,#31993,#31994,#31995,#31996,#31997,#31998,#31999,#32000,#32001,
#32002,#32003,#32004,#32005,#32006,#32007,#32008,#32009,#32010,#32011,#32012,
#32013,#32014,#32015,#32016,#32017,#32018,#32019,#32020,#32021,#32022,#32023,
#32024,#32025,#32026,#32027,#32028,#32029,#32030,#32031,#32032,#32033,#32034,
#32035,#32036,#32037,#32038,#32039,#32040,#32041,#32042,#32043,#32044,#32045,
#32046,#32047,#32048,#32049,#32050,#32051,#32052,#32053,#32054,#32055,#32056,
#32057,#32058,#32059,#32060,#32061,#32062,#32063,#32064,#32065,#32066,#32067,
#32068,#32069,#32070,#32071,#32072,#32073,#32074,#32075,#32076,#32077,#32078,
#32079,#32080,#32081,#32082,#32083,#32084),(#32085,#32086,#32087,#32088,
#32089,#32090,#32091,#32092,#32093,#32094,#32095,#32096,#32097,#32098,#32099,
#32100,#32101,#32102,#32103,#32104,#32105,#32106,#32107,#32108,#32109,#32110,
#32111,#32112,#32113,#32114,#32115,#32116,#32117,#32118,#32119,#32120,#32121,
#32122,#32123,#32124,#32125,#32126,#32127,#32128,#32129,#32130,#32131,#32132,
#32133,#32134,#32135,#32136,#32137,#32138,#32139,#32140,#32141,#32142,#32143,
#32144,#32145,#32146,#32147,#32148,#32149,#32150,#32151,#32152,#32153,#32154,
#32155,#32156,#32157,#32158,#32159,#32160,#32161,#32162,#32163,#32164,#32165,
#32166,#32167,#32168,#32169,#32170,#32171,#32172,#32173,#32174,#32175,#32176,
#32177,#32178,#32179,#32180,#32181,#32182,#32183,#32184,#32185,#32186,#32187,
#32188,#32189,#32190,#32191,#32192,#32193,#32194,#32195,#32196,#32197,#32198,
#32199),(#32200,#32201,#32202,#32203,#32204,#32205,#32206,#32207,#32208,
#32209,#32210,#32211,#32212,#32213,#32214,#32215,#32216,#32217,#32218,#32219,
#32220,#32221,#32222,#32223,#32224,#32225,#32226,#32227,#32228,#32229,#32230,
#32231,#32232,#32233,#32234,#32235,#32236,#32237,#32238,#32239,#32240,#32241,
#32242,#32243,#32244,#32245,#32246,#32247,#32248,#32249,#32250,#32251,#32252,
#32253,#32254,#32255,#32256,#32257,#32258,#32259,#32260,#32261,#32262,#32263,
#32264,#32265,#32266,#32267,#32268,#32269,#32270,#32271,#32272,#32273,#32274,
#32275,#32276,#32277,#32278,#32279,#32280,#32281,#32282,#32283,#32284,#32285,
#32286,#32287,#32288,#32289,#32290,#32291,#32292,#32293,#32294,#32295,#32296,
#32297,#32298,#32299,#32300,#32301,#32302,#32303,#32304,#32305,#32306,#32307,
#32308,#32309,#32310,#32311,#32312,#32313,#32314)),.UNSPECIFIED.,.F.,.F.,
 .F.,(4,4),(4,1,1,1,1,1,1,1,1,1,1,1,1,1,1,1,1,1,1,1,1,1,1,1,1,1,1,1,1,1,
1,1,1,1,1,1,1,1,1,1,1,1,1,1,1,1,1,1,1,1,1,1,1,1,1,1,1,1,1,1,1,1,1,1,1,1,
1,1,1,1,1,1,1,1,1,1,1,1,1,1,1,1,1,1,1,1,1,1,1,1,1,1,1,1,1,1,1,1,1,1,1,1,
1,1,1,1,1,1,1,1,1,1,4),(0.,0.173020531651036),(12.1475814751569,12.6421543672732,
13.1367272593894,13.6313001515056,14.1258730436219,14.6204459357381,15.1150188278544,
15.6095917199706,16.1041646120869,16.5987375042031,17.0933103963194,17.5878832884356,
18.0824561805519,18.5770290726681,19.0716019647843,19.5661748569006,20.0607477490168,
20.5553206411331,21.0498935332493,21.5444664253656,22.0390393174818,22.5336122095981,
23.0281851017143,23.5227579938306,24.0173308859468,24.511903778063,25.0064766701793,
25.5010495622955,25.9956224544118,26.490195346528,26.9847682386443,27.4793411307605,
27.9739140228768,28.468486914993,28.9630598071093,29.4576326992255,29.9522055913417,
30.446778483458,30.9413513755742,31.4359242676905,31.9304971598067,32.425070051923,
32.9196429440392,33.4142158361555,33.9087887282717,34.403361620388,34.8979345125042,
35.3925074046204,35.8870802967367,36.3816531888529,36.8762260809692,37.3707989730854,
37.8653718652017,38.3599447573179,38.8545176494342,39.3490905415504,39.8436634336667,
40.3382363257829,40.8328092178991,41.3273821100154,41.8219550021316,42.3165278942479,
42.8111007863641,43.3056736784804,43.8002465705966,44.2948194627129,44.7893923548291,
45.2839652469454,45.7785381390616,46.2731110311778,46.7676839232941,47.2622568154103,
47.7568297075266,48.2514025996428,48.7459754917591,49.2405483838753,49.7351212759916,
50.2296941681078,50.7242670602241,51.2188399523403,51.7134128444565,52.2079857365728,
52.702558628689,53.1971315208053,53.6917044129215,54.1862773050378,54.680850197154,
55.1754230892703,55.6699959813865,56.1645688735028,56.659141765619,57.1537146577353,
57.6482875498515,58.1428604419677,58.637433334084,59.1320062262002,59.6265791183165,
60.1211520104327,60.615724902549,61.1102977946652,61.6048706867815,62.0994435788977,
62.5940164710139,63.0885893631302,63.5831622552464,64.0777351473627,64.5723080394789,
65.0668809315952,65.5614538237114,66.0560267158277,66.5505996079439,67.0451725000601,
67.5397453921764),.UNSPECIFIED.);
#12=B_SPLINE_SURFACE_WITH_KNOTS('',3,3,((#32414,#32415,#32416,#32417,#32418,
#32419,#32420,#32421,#32422,#32423,#32424,#32425,#32426,#32427,#32428,#32429,
#32430,#32431,#32432,#32433,#32434,#32435,#32436,#32437,#32438,#32439,#32440,
#32441,#32442,#32443,#32444,#32445,#32446,#32447,#32448,#32449,#32450,#32451,
#32452,#32453,#32454,#32455,#32456,#32457,#32458,#32459,#32460,#32461,#32462,
#32463,#32464,#32465,#32466,#32467,#32468,#32469,#32470,#32471,#32472,#32473,
#32474,#32475,#32476,#32477,#32478,#32479,#32480,#32481,#32482,#32483,#32484,
#32485,#32486,#32487,#32488,#32489,#32490,#32491,#32492,#32493,#32494,#32495,
#32496,#32497,#32498,#32499,#32500,#32501,#32502,#32503,#32504,#32505,#32506,
#32507,#32508,#32509,#32510,#32511,#32512,#32513,#32514,#32515,#32516,#32517,
#32518,#32519,#32520,#32521,#32522,#32523,#32524,#32525,#32526,#32527,#32528),
(#32529,#32530,#32531,#32532,#32533,#32534,#32535,#32536,#32537,#32538,
#32539,#32540,#32541,#32542,#32543,#32544,#32545,#32546,#32547,#32548,#32549,
#32550,#32551,#32552,#32553,#32554,#32555,#32556,#32557,#32558,#32559,#32560,
#32561,#32562,#32563,#32564,#32565,#32566,#32567,#32568,#32569,#32570,#32571,
#32572,#32573,#32574,#32575,#32576,#32577,#32578,#32579,#32580,#32581,#32582,
#32583,#32584,#32585,#32586,#32587,#32588,#32589,#32590,#32591,#32592,#32593,
#32594,#32595,#32596,#32597,#32598,#32599,#32600,#32601,#32602,#32603,#32604,
#32605,#32606,#32607,#32608,#32609,#32610,#32611,#32612,#32613,#32614,#32615,
#32616,#32617,#32618,#32619,#32620,#32621,#32622,#32623,#32624,#32625,#32626,
#32627,#32628,#32629,#32630,#32631,#32632,#32633,#32634,#32635,#32636,#32637,
#32638,#32639,#32640,#32641,#32642,#32643),(#32644,#32645,#32646,#32647,
#32648,#32649,#32650,#32651,#32652,#32653,#32654,#32655,#32656,#32657,#32658,
#32659,#32660,#32661,#32662,#32663,#32664,#32665,#32666,#32667,#32668,#32669,
#32670,#32671,#32672,#32673,#32674,#32675,#32676,#32677,#32678,#32679,#32680,
#32681,#32682,#32683,#32684,#32685,#32686,#32687,#32688,#32689,#32690,#32691,
#32692,#32693,#32694,#32695,#32696,#32697,#32698,#32699,#32700,#32701,#32702,
#32703,#32704,#32705,#32706,#32707,#32708,#32709,#32710,#32711,#32712,#32713,
#32714,#32715,#32716,#32717,#32718,#32719,#32720,#32721,#32722,#32723,#32724,
#32725,#32726,#32727,#32728,#32729,#32730,#32731,#32732,#32733,#32734,#32735,
#32736,#32737,#32738,#32739,#32740,#32741,#32742,#32743,#32744,#32745,#32746,
#32747,#32748,#32749,#32750,#32751,#32752,#32753,#32754,#32755,#32756,#32757,
#32758),(#32759,#32760,#32761,#32762,#32763,#32764,#32765,#32766,#32767,
#32768,#32769,#32770,#32771,#32772,#32773,#32774,#32775,#32776,#32777,#32778,
#32779,#32780,#32781,#32782,#32783,#32784,#32785,#32786,#32787,#32788,#32789,
#32790,#32791,#32792,#32793,#32794,#32795,#32796,#32797,#32798,#32799,#32800,
#32801,#32802,#32803,#32804,#32805,#32806,#32807,#32808,#32809,#32810,#32811,
#32812,#32813,#32814,#32815,#32816,#32817,#32818,#32819,#32820,#32821,#32822,
#32823,#32824,#32825,#32826,#32827,#32828,#32829,#32830,#32831,#32832,#32833,
#32834,#32835,#32836,#32837,#32838,#32839,#32840,#32841,#32842,#32843,#32844,
#32845,#32846,#32847,#32848,#32849,#32850,#32851,#32852,#32853,#32854,#32855,
#32856,#32857,#32858,#32859,#32860,#32861,#32862,#32863,#32864,#32865,#32866,
#32867,#32868,#32869,#32870,#32871,#32872,#32873)),.UNSPECIFIED.,.F.,.F.,
 .F.,(4,4),(4,1,1,1,1,1,1,1,1,1,1,1,1,1,1,1,1,1,1,1,1,1,1,1,1,1,1,1,1,1,
1,1,1,1,1,1,1,1,1,1,1,1,1,1,1,1,1,1,1,1,1,1,1,1,1,1,1,1,1,1,1,1,1,1,1,1,
1,1,1,1,1,1,1,1,1,1,1,1,1,1,1,1,1,1,1,1,1,1,1,1,1,1,1,1,1,1,1,1,1,1,1,1,
1,1,1,1,1,1,1,1,1,1,4),(0.,0.173020531651036),(15.1888611523549,15.6834340444711,
16.1780069365874,16.6725798287036,17.1671527208199,17.6617256129361,18.1562985050523,
18.6508713971686,19.1454442892848,19.6400171814011,20.1345900735173,20.6291629656336,
21.1237358577498,21.6183087498661,22.1128816419823,22.6074545340986,23.1020274262148,
23.596600318331,24.0911732104473,24.5857461025635,25.0803189946798,25.574891886796,
26.0694647789123,26.5640376710285,27.0586105631448,27.553183455261,28.0477563473773,
28.5423292394935,29.0369021316097,29.531475023726,30.0260479158422,30.5206208079585,
31.0151937000747,31.509766592191,32.0043394843072,32.4989123764235,32.9934852685397,
33.488058160656,33.9826310527722,34.4772039448884,34.9717768370047,35.4663497291209,
35.9609226212372,36.4554955133534,36.9500684054697,37.4446412975859,37.9392141897022,
38.4337870818184,38.9283599739347,39.4229328660509,39.9175057581671,40.4120786502834,
40.9066515423996,41.4012244345159,41.8957973266321,42.3903702187484,42.8849431108646,
43.3795160029809,43.8740888950971,44.3686617872134,44.8632346793296,45.3578075714458,
45.8523804635621,46.3469533556783,46.8415262477946,47.3360991399108,47.8306720320271,
48.3252449241433,48.8198178162596,49.3143907083758,49.8089636004921,50.3035364926083,
50.7981093847245,51.2926822768408,51.787255168957,52.2818280610733,52.7764009531895,
53.2709738453058,53.765546737422,54.2601196295383,54.7546925216545,55.2492654137708,
55.743838305887,56.2384111980032,56.7329840901195,57.2275569822357,57.722129874352,
58.2167027664682,58.7112756585845,59.2058485507007,59.700421442817,60.1949943349332,
60.6895672270495,61.1841401191657,61.6787130112819,62.1732859033982,62.6678587955144,
63.1624316876307,63.6570045797469,64.1515774718632,64.6461503639794,65.1407232560957,
65.6352961482119,66.1298690403281,66.6244419324444,67.1190148245607,67.6135877166769,
68.1081606087931,68.6027335009094,69.0973063930256,69.5918792851419,70.0864521772581,
70.5810250693744),.UNSPECIFIED.);
#585=B_SPLINE_CURVE_WITH_KNOTS('',3,(#30811,#30812,#30813,#30814,#30815,
#30816,#30817,#30818,#30819,#30820,#30821,#30822,#30823,#30824,#30825,#30826,
#30827,#30828,#30829,#30830,#30831,#30832,#30833,#30834,#30835),
 .UNSPECIFIED.,.F.,.F.,(4,3,3,3,3,3,3,3,4),(-3.56038179279204,-3.46201024481372,
-2.96743735269747,-2.47286446058123,-1.97829156846498,-1.48371867634874,
-0.989145784232491,-0.494572892116246,0.),.UNSPECIFIED.);
#586=B_SPLINE_CURVE_WITH_KNOTS('',3,(#30838,#30839,#30840,#30841,#30842,
#30843,#30844,#30845,#30846,#30847,#30848,#30849,#30850,#30851,#30852,#30853,
#30854,#30855,#30856,#30857,#30858,#30859,#30860,#30861,#30862,#30863,#30864,
#30865,#30866,#30867,#30868,#30869,#30870,#30871,#30872,#30873,#30874,#30875,
#30876,#30877),.UNSPECIFIED.,.F.,.F.,(4,3,3,3,3,3,3,3,3,3,3,3,3,4),(0.937891254796418,
0.989145784232494,1.48371867634874,1.97829156846498,2.47286446058123,2.96743735269748,
3.46201024481372,3.95658313692997,4.45115602904621,4.94572892116246,5.44030181327871,
5.93487470539495,6.42944759751119,6.80228742277363),.UNSPECIFIED.);
#587=B_SPLINE_CURVE_WITH_KNOTS('',3,(#30882,#30883,#30884,#30885,#30886,
#30887,#30888,#30889,#30890,#30891,#30892,#30893,#30894,#30895,#30896,#30897,
#30898,#30899,#30900,#30901,#30902,#30903,#30904,#30905,#30906,#30907,#30908,
#30909,#30910,#30911,#30912,#30913,#30914,#30915,#30916,#30917,#30918,#30919,
#30920,#30921),.UNSPECIFIED.,.F.,.F.,(4,3,3,3,3,3,3,3,3,3,3,3,3,4),(-9.8435670999716,
-9.39688495020867,-8.90231205809242,-8.40773916597618,-7.91316627385993,
-7.41859338174369,-6.92402048962744,-6.42944759751119,-5.93487470539495,
-5.4403018132787,-4.94572892116246,-4.45115602904621,-3.95658313692996,
-3.56038179279204),.UNSPECIFIED.);
#588=B_SPLINE_CURVE_WITH_KNOTS('',3,(#30922,#30923,#30924,#30925,#30926,
#30927,#30928,#30929,#30930,#30931,#30932,#30933,#30934,#30935,#30936,#30937,
#30938,#30939,#30940,#30941,#30942,#30943,#30944,#30945,#30946,#30947,#30948,
#30949,#30950,#30951,#30952,#30953,#30954,#30955,#30956,#30957,#30958,#30959,
#30960,#30961,#30962,#30963,#30964),.UNSPECIFIED.,.F.,.F.,(4,3,3,3,3,3,
3,3,3,3,3,3,3,3,4),(6.80228742277363,6.92402048962744,7.41859338174369,
7.91316627385993,8.40773916597617,8.90231205809242,9.39688495020867,9.89145784232491,
10.3860307344412,10.8806036265574,11.3751765186736,11.8697494107899,12.3643223029061,
12.8588951950224,13.0854727299532),.UNSPECIFIED.);
#589=B_SPLINE_CURVE_WITH_KNOTS('',3,(#30969,#30970,#30971,#30972,#30973,
#30974,#30975,#30976,#30977,#30978,#30979,#30980,#30981,#30982,#30983,#30984,
#30985,#30986,#30987,#30988,#30989,#30990,#30991,#30992,#30993,#30994,#30995,
#30996,#30997,#30998,#30999,#31000,#31001,#31002,#31003,#31004,#31005,#31006,
#31007,#31008,#31009,#31010,#31011),.UNSPECIFIED.,.F.,.F.,(4,3,3,3,3,3,
3,3,3,3,3,3,3,3,4),(-16.1267524071512,-15.8263325477199,-15.3317596556036,
-14.8371867634874,-14.3426138713711,-13.8480409792549,-13.3534680871386,
-12.8588951950224,-12.3643223029061,-11.8697494107899,-11.3751765186736,
-10.8806036265574,-10.3860307344412,-9.89145784232491,-9.8435670999716),
 .UNSPECIFIED.);
#590=B_SPLINE_CURVE_WITH_KNOTS('',3,(#31012,#31013,#31014,#31015,#31016,
#31017,#31018,#31019,#31020,#31021,#31022,#31023,#31024,#31025,#31026,#31027,
#31028,#31029,#31030,#31031,#31032,#31033,#31034,#31035,#31036,#31037,#31038,
#31039,#31040,#31041,#31042,#31043,#31044,#31045,#31046,#31047,#31048,#31049,
#31050,#31051,#31052,#31053,#31054),.UNSPECIFIED.,.F.,.F.,(4,3,3,3,3,3,
3,3,3,3,3,3,3,3,4),(13.0854727299532,13.3534680871386,13.8480409792549,
14.3426138713711,14.8371867634874,15.3317596556036,15.8263325477199,16.3209054398361,
16.8154783319523,17.3100512240686,17.8046241161848,18.2991970083011,18.7937699004173,
19.2883427925336,19.3686580371328),.UNSPECIFIED.);
#591=B_SPLINE_CURVE_WITH_KNOTS('',3,(#31059,#31060,#31061,#31062,#31063,
#31064,#31065,#31066,#31067,#31068,#31069,#31070,#31071,#31072,#31073,#31074,
#31075,#31076,#31077,#31078,#31079,#31080,#31081,#31082,#31083,#31084,#31085,
#31086,#31087,#31088,#31089,#31090,#31091,#31092,#31093,#31094,#31095,#31096,
#31097,#31098,#31099,#31100,#31101),.UNSPECIFIED.,.F.,.F.,(4,3,3,3,3,3,
3,3,3,3,3,3,3,3,4),(-22.4099377143308,-22.2557801452311,-21.7612072531148,
-21.2666343609986,-20.7720614688823,-20.2774885767661,-19.7829156846498,
-19.2883427925336,-18.7937699004173,-18.2991970083011,-17.8046241161848,
-17.3100512240686,-16.8154783319523,-16.3209054398361,-16.1267524071512),
 .UNSPECIFIED.);
#592=B_SPLINE_CURVE_WITH_KNOTS('',3,(#31102,#31103,#31104,#31105,#31106,
#31107,#31108,#31109,#31110,#31111,#31112,#31113,#31114,#31115,#31116,#31117,
#31118,#31119,#31120,#31121,#31122,#31123,#31124,#31125,#31126,#31127,#31128,
#31129,#31130,#31131,#31132,#31133,#31134,#31135,#31136,#31137,#31138,#31139,
#31140,#31141),.UNSPECIFIED.,.F.,.F.,(4,3,3,3,3,3,3,3,3,3,3,3,3,4),(19.3686580371328,
19.7829156846498,20.2774885767661,20.7720614688823,21.2666343609986,21.7612072531148,
22.255780145231,22.7503530373473,23.2449259294635,23.7394988215798,24.234071713696,
24.7286446058123,25.2232174979285,25.6518433443124),.UNSPECIFIED.);
#593=B_SPLINE_CURVE_WITH_KNOTS('',3,(#31146,#31147,#31148,#31149,#31150,
#31151,#31152,#31153,#31154,#31155,#31156,#31157,#31158,#31159,#31160,#31161,
#31162,#31163,#31164,#31165,#31166,#31167,#31168,#31169,#31170,#31171,#31172,
#31173,#31174,#31175,#31176,#31177,#31178,#31179,#31180,#31181,#31182,#31183,
#31184,#31185,#31186,#31187,#31188),.UNSPECIFIED.,.F.,.F.,(4,3,3,3,3,3,
3,3,3,3,3,3,3,3,4),(-28.6931230215104,-28.6852277427422,-28.190654850626,
-27.6960819585097,-27.2015090663935,-26.7069361742773,-26.212363282161,
-25.7177903900448,-25.2232174979285,-24.7286446058123,-24.234071713696,
-23.7394988215798,-23.2449259294635,-22.7503530373473,-22.4099377143308),
 .UNSPECIFIED.);
#594=B_SPLINE_CURVE_WITH_KNOTS('',3,(#31189,#31190,#31191,#31192,#31193,
#31194,#31195,#31196,#31197,#31198,#31199,#31200,#31201,#31202,#31203,#31204,
#31205,#31206,#31207,#31208,#31209,#31210,#31211,#31212,#31213,#31214,#31215,
#31216,#31217,#31218,#31219,#31220,#31221,#31222,#31223,#31224,#31225,#31226,
#31227,#31228,#31229,#31230,#31231),.UNSPECIFIED.,.F.,.F.,(4,3,3,3,3,3,
3,3,3,3,3,3,3,3,4),(25.6518433443124,25.7177903900448,26.212363282161,26.7069361742773,
27.2015090663935,27.6960819585097,28.190654850626,28.6852277427422,29.1798006348585,
29.6743735269747,30.168946419091,30.6635193112072,31.1580922033235,31.6526650954397,
31.935028651492),.UNSPECIFIED.);
#595=B_SPLINE_CURVE_WITH_KNOTS('',3,(#31236,#31237,#31238,#31239,#31240,
#31241,#31242,#31243,#31244,#31245,#31246,#31247,#31248,#31249,#31250,#31251,
#31252,#31253,#31254,#31255,#31256,#31257,#31258,#31259,#31260,#31261,#31262,
#31263,#31264,#31265,#31266,#31267,#31268,#31269,#31270,#31271,#31272,#31273,
#31274,#31275),.UNSPECIFIED.,.F.,.F.,(4,3,3,3,3,3,3,3,3,3,3,3,3,4),(-34.97630832869,
-34.6201024481372,-34.1255295560209,-33.6309566639047,-33.1363837717884,
-32.6418108796722,-32.147237987556,-31.6526650954397,-31.1580922033235,
-30.6635193112072,-30.168946419091,-29.6743735269747,-29.1798006348585,
-28.6931230215104),.UNSPECIFIED.);
#596=B_SPLINE_CURVE_WITH_KNOTS('',3,(#31276,#31277,#31278,#31279,#31280,
#31281,#31282,#31283,#31284,#31285,#31286,#31287,#31288,#31289,#31290,#31291,
#31292,#31293,#31294,#31295,#31296,#31297,#31298,#31299,#31300,#31301,#31302,
#31303,#31304,#31305,#31306,#31307,#31308,#31309,#31310,#31311,#31312,#31313,
#31314,#31315,#31316,#31317,#31318),.UNSPECIFIED.,.F.,.F.,(4,3,3,3,3,3,
3,3,3,3,3,3,3,3,4),(31.935028651492,32.147237987556,32.6418108796722,33.1363837717885,
33.6309566639047,34.1255295560209,34.6201024481372,35.1146753402534,35.6092482323697,
36.1038211244859,36.5983940166022,37.0929669087184,37.5875398008347,38.0821126929509,
38.2182139586716),.UNSPECIFIED.);
#597=B_SPLINE_CURVE_WITH_KNOTS('',3,(#31323,#31324,#31325,#31326,#31327,
#31328,#31329,#31330,#31331,#31332,#31333,#31334,#31335,#31336,#31337,#31338,
#31339,#31340,#31341,#31342,#31343,#31344,#31345,#31346,#31347,#31348,#31349,
#31350,#31351,#31352,#31353,#31354,#31355,#31356,#31357,#31358,#31359,#31360,
#31361,#31362,#31363,#31364,#31365),.UNSPECIFIED.,.F.,.F.,(4,3,3,3,3,3,
3,3,3,3,3,3,3,3,4),(-41.2594936358696,-41.0495500456484,-40.5549771535321,
-40.0604042614159,-39.5658313692996,-39.0712584771834,-38.5766855850671,
-38.0821126929509,-37.5875398008347,-37.0929669087184,-36.5983940166022,
-36.1038211244859,-35.6092482323697,-35.1146753402534,-34.97630832869),
 .UNSPECIFIED.);
#598=B_SPLINE_CURVE_WITH_KNOTS('',3,(#31366,#31367,#31368,#31369,#31370,
#31371,#31372,#31373,#31374,#31375,#31376,#31377,#31378,#31379,#31380,#31381,
#31382,#31383,#31384,#31385,#31386,#31387,#31388,#31389,#31390,#31391,#31392,
#31393,#31394,#31395,#31396,#31397,#31398,#31399,#31400,#31401,#31402,#31403,
#31404,#31405),.UNSPECIFIED.,.F.,.F.,(4,3,3,3,3,3,3,3,3,3,3,3,3,4),(38.2182139586716,
38.5766855850671,39.0712584771834,39.5658313692996,40.0604042614159,40.5549771535321,
41.0495500456484,41.5441229377646,42.0386958298809,42.5332687219971,43.0278416141134,
43.5224145062296,44.0169873983459,44.5013992658512),.UNSPECIFIED.);
#599=B_SPLINE_CURVE_WITH_KNOTS('',3,(#31410,#31411,#31412,#31413,#31414,
#31415,#31416,#31417,#31418,#31419,#31420,#31421,#31422,#31423,#31424,#31425,
#31426,#31427,#31428,#31429,#31430,#31431,#31432,#31433,#31434,#31435,#31436,
#31437,#31438,#31439,#31440,#31441,#31442,#31443,#31444,#31445,#31446,#31447,
#31448,#31449,#31450,#31451,#31452),.UNSPECIFIED.,.F.,.F.,(4,3,3,3,3,3,
3,3,3,3,3,3,3,3,4),(-47.5426789430491,-47.4789976431596,-46.9844247510433,
-46.4898518589271,-45.9952789668108,-45.5007060746946,-45.0061331825783,
-44.5115602904621,-44.0169873983458,-43.5224145062296,-43.0278416141134,
-42.5332687219971,-42.0386958298809,-41.5441229377646,-41.2594936358696),
 .UNSPECIFIED.);
#600=B_SPLINE_CURVE_WITH_KNOTS('',3,(#31453,#31454,#31455,#31456,#31457,
#31458,#31459,#31460,#31461,#31462,#31463,#31464,#31465,#31466,#31467,#31468,
#31469,#31470,#31471,#31472,#31473,#31474,#31475,#31476,#31477,#31478,#31479,
#31480,#31481,#31482,#31483,#31484,#31485,#31486,#31487,#31488,#31489,#31490,
#31491,#31492,#31493,#31494,#31495),.UNSPECIFIED.,.F.,.F.,(4,3,3,3,3,3,
3,3,3,3,3,3,3,3,4),(44.5013992658512,44.5115602904621,45.0061331825783,
45.5007060746946,45.9952789668108,46.4898518589271,46.9844247510433,47.4789976431596,
47.9735705352758,48.4681434273921,48.9627163195083,49.4572892116245,49.9518621037408,
50.446434995857,50.7845845730308),.UNSPECIFIED.);
#601=B_SPLINE_CURVE_WITH_KNOTS('',3,(#31502,#31503,#31504,#31505,#31506,
#31507,#31508,#31509,#31510,#31511),.UNSPECIFIED.,.F.,.F.,(4,3,3,4),(-54.4542726622231,
-54.403018132787,-53.9084452406708,-53.8258642502287),.UNSPECIFIED.);
#602=B_SPLINE_CURVE_WITH_KNOTS('',3,(#31517,#31518,#31519,#31520,#31521,
#31522,#31523),.UNSPECIFIED.,.F.,.F.,(4,1,1,1,4),(65.9734457253856,66.0560267158277,
66.5505996079439,67.0451725000601,67.5397453921764),.UNSPECIFIED.);
#603=B_SPLINE_CURVE_WITH_KNOTS('',3,(#31526,#31527,#31528,#31529,#31530,
#31531,#31532,#31533,#31534,#31535,#31536,#31537),.UNSPECIFIED.,.F.,.F.,
(4,1,1,1,1,1,1,1,1,4),(65.9734457253856,66.1298690403281,66.6244419324444,
67.1190148245607,67.6135877166769,68.1081606087931,68.6027335009094,69.0973063930256,
69.5918792851419,69.643133814578),.UNSPECIFIED.);
#604=B_SPLINE_CURVE_WITH_KNOTS('',3,(#31542,#31543,#31544,#31545,#31546,
#31547,#31548,#31549,#31550,#31551,#31552,#31553,#31554,#31555,#31556,#31557),
 .UNSPECIFIED.,.F.,.F.,(4,1,1,1,1,1,1,1,1,1,1,1,1,4),(59.6902604182061,
60.1211520104327,60.615724902549,61.1102977946652,61.6048706867815,62.0994435788977,
62.5940164710139,63.0885893631302,63.5831622552464,64.0777351473627,64.5723080394789,
65.0668809315952,65.5614538237114,65.9734457253856),.UNSPECIFIED.);
#605=B_SPLINE_CURVE_WITH_KNOTS('',3,(#31558,#31559,#31560,#31561,#31562,
#31563,#31564,#31565,#31566,#31567,#31568,#31569,#31570,#31571,#31572,#31573,
#31574),.UNSPECIFIED.,.F.,.F.,(4,1,1,1,1,1,1,1,1,1,1,1,1,1,4),(59.6902604182061,
59.700421442817,60.1949943349332,60.6895672270495,61.1841401191657,61.6787130112819,
62.1732859033982,62.6678587955144,63.1624316876307,63.6570045797469,64.1515774718632,
64.6461503639794,65.1407232560957,65.6352961482119,65.9734457253856),
 .UNSPECIFIED.);
#606=B_SPLINE_CURVE_WITH_KNOTS('',3,(#31579,#31580,#31581,#31582,#31583,
#31584,#31585,#31586,#31587,#31588,#31589,#31590,#31591,#31592,#31593,#31594,
#31595),.UNSPECIFIED.,.F.,.F.,(4,1,1,1,1,1,1,1,1,1,1,1,1,1,4),(53.4070751110264,
53.6917044129215,54.1862773050378,54.680850197154,55.1754230892703,55.6699959813865,
56.1645688735028,56.659141765619,57.1537146577353,57.6482875498515,58.1428604419677,
58.637433334084,59.1320062262002,59.6265791183165,59.6902604182061),
 .UNSPECIFIED.);
#607=B_SPLINE_CURVE_WITH_KNOTS('',3,(#31596,#31597,#31598,#31599,#31600,
#31601,#31602,#31603,#31604,#31605,#31606,#31607,#31608,#31609,#31610,#31611),
 .UNSPECIFIED.,.F.,.F.,(4,1,1,1,1,1,1,1,1,1,1,1,1,4),(53.4070751110264,
53.765546737422,54.2601196295383,54.7546925216545,55.2492654137708,55.743838305887,
56.2384111980032,56.7329840901195,57.2275569822357,57.722129874352,58.2167027664682,
58.7112756585845,59.2058485507007,59.6902604182061),.UNSPECIFIED.);
#608=B_SPLINE_CURVE_WITH_KNOTS('',3,(#31616,#31617,#31618,#31619,#31620,
#31621,#31622,#31623,#31624,#31625,#31626,#31627,#31628,#31629,#31630,#31631,
#31632),.UNSPECIFIED.,.F.,.F.,(4,1,1,1,1,1,1,1,1,1,1,1,1,1,4),(47.1238898038469,
47.2622568154103,47.7568297075266,48.2514025996428,48.7459754917591,49.2405483838753,
49.7351212759916,50.2296941681078,50.7242670602241,51.2188399523403,51.7134128444565,
52.2079857365728,52.702558628689,53.1971315208053,53.4070751110264),
 .UNSPECIFIED.);
#609=B_SPLINE_CURVE_WITH_KNOTS('',3,(#31633,#31634,#31635,#31636,#31637,
#31638,#31639,#31640,#31641,#31642,#31643,#31644,#31645,#31646,#31647,#31648,
#31649),.UNSPECIFIED.,.F.,.F.,(4,1,1,1,1,1,1,1,1,1,1,1,1,1,4),(47.1238898038469,
47.3360991399108,47.8306720320271,48.3252449241433,48.8198178162596,49.3143907083758,
49.8089636004921,50.3035364926083,50.7981093847245,51.2926822768408,51.787255168957,
52.2818280610733,52.7764009531895,53.2709738453058,53.4070751110264),
 .UNSPECIFIED.);
#610=B_SPLINE_CURVE_WITH_KNOTS('',3,(#31654,#31655,#31656,#31657,#31658,
#31659,#31660,#31661,#31662,#31663,#31664,#31665,#31666,#31667,#31668,#31669),
 .UNSPECIFIED.,.F.,.F.,(4,1,1,1,1,1,1,1,1,1,1,1,1,4),(40.8407044966673,
41.3273821100154,41.8219550021316,42.3165278942479,42.8111007863641,43.3056736784804,
43.8002465705966,44.2948194627129,44.7893923548291,45.2839652469454,45.7785381390616,
46.2731110311778,46.7676839232941,47.1238898038469),.UNSPECIFIED.);
#611=B_SPLINE_CURVE_WITH_KNOTS('',3,(#31670,#31671,#31672,#31673,#31674,
#31675,#31676,#31677,#31678,#31679,#31680,#31681,#31682,#31683,#31684,#31685,
#31686),.UNSPECIFIED.,.F.,.F.,(4,1,1,1,1,1,1,1,1,1,1,1,1,1,4),(40.8407044966673,
40.9066515423996,41.4012244345159,41.8957973266321,42.3903702187484,42.8849431108646,
43.3795160029809,43.8740888950971,44.3686617872134,44.8632346793296,45.3578075714458,
45.8523804635621,46.3469533556783,46.8415262477946,47.1238898038469),
 .UNSPECIFIED.);
#612=B_SPLINE_CURVE_WITH_KNOTS('',3,(#31691,#31692,#31693,#31694,#31695,
#31696,#31697,#31698,#31699,#31700,#31701,#31702,#31703,#31704,#31705,#31706,
#31707),.UNSPECIFIED.,.F.,.F.,(4,1,1,1,1,1,1,1,1,1,1,1,1,1,4),(34.5575191894877,
34.8979345125042,35.3925074046204,35.8870802967367,36.3816531888529,36.8762260809692,
37.3707989730854,37.8653718652017,38.3599447573179,38.8545176494342,39.3490905415504,
39.8436634336667,40.3382363257829,40.8328092178991,40.8407044966673),
 .UNSPECIFIED.);
#613=B_SPLINE_CURVE_WITH_KNOTS('',3,(#31708,#31709,#31710,#31711,#31712,
#31713,#31714,#31715,#31716,#31717,#31718,#31719,#31720,#31721,#31722,#31723),
 .UNSPECIFIED.,.F.,.F.,(4,1,1,1,1,1,1,1,1,1,1,1,1,4),(34.5575191894877,
34.9717768370047,35.4663497291209,35.9609226212372,36.4554955133534,36.9500684054697,
37.4446412975859,37.9392141897022,38.4337870818184,38.9283599739347,39.4229328660509,
39.9175057581671,40.4120786502834,40.8407044966673),.UNSPECIFIED.);
#614=B_SPLINE_CURVE_WITH_KNOTS('',3,(#31728,#31729,#31730,#31731,#31732,
#31733,#31734,#31735,#31736,#31737,#31738,#31739,#31740,#31741,#31742,#31743,
#31744),.UNSPECIFIED.,.F.,.F.,(4,1,1,1,1,1,1,1,1,1,1,1,1,1,4),(28.2743338823081,
28.468486914993,28.9630598071093,29.4576326992255,29.9522055913417,30.446778483458,
30.9413513755742,31.4359242676905,31.9304971598067,32.425070051923,32.9196429440392,
33.4142158361555,33.9087887282717,34.403361620388,34.5575191894877),
 .UNSPECIFIED.);
#615=B_SPLINE_CURVE_WITH_KNOTS('',3,(#31745,#31746,#31747,#31748,#31749,
#31750,#31751,#31752,#31753,#31754,#31755,#31756,#31757,#31758,#31759,#31760,
#31761),.UNSPECIFIED.,.F.,.F.,(4,1,1,1,1,1,1,1,1,1,1,1,1,1,4),(28.2743338823081,
28.5423292394935,29.0369021316097,29.531475023726,30.0260479158422,30.5206208079585,
31.0151937000747,31.509766592191,32.0043394843072,32.4989123764235,32.9934852685397,
33.488058160656,33.9826310527722,34.4772039448884,34.5575191894877),
 .UNSPECIFIED.);
#616=B_SPLINE_CURVE_WITH_KNOTS('',3,(#31766,#31767,#31768,#31769,#31770,
#31771,#31772,#31773,#31774,#31775,#31776,#31777,#31778,#31779,#31780,#31781,
#31782),.UNSPECIFIED.,.F.,.F.,(4,1,1,1,1,1,1,1,1,1,1,1,1,1,4),(21.9911485751285,
22.0390393174818,22.5336122095981,23.0281851017143,23.5227579938306,24.0173308859468,
24.511903778063,25.0064766701793,25.5010495622955,25.9956224544118,26.490195346528,
26.9847682386443,27.4793411307605,27.9739140228768,28.2743338823081),
 .UNSPECIFIED.);
#617=B_SPLINE_CURVE_WITH_KNOTS('',3,(#31783,#31784,#31785,#31786,#31787,
#31788,#31789,#31790,#31791,#31792,#31793,#31794,#31795,#31796,#31797,#31798,
#31799),.UNSPECIFIED.,.F.,.F.,(4,1,1,1,1,1,1,1,1,1,1,1,1,1,4),(21.9911485751285,
22.1128816419823,22.6074545340986,23.1020274262148,23.596600318331,24.0911732104473,
24.5857461025635,25.0803189946798,25.574891886796,26.0694647789123,26.5640376710285,
27.0586105631448,27.553183455261,28.0477563473773,28.2743338823081),
 .UNSPECIFIED.);
#618=B_SPLINE_CURVE_WITH_KNOTS('',3,(#31805,#31806,#31807,#31808,#31809),
 .UNSPECIFIED.,.F.,.F.,(4,1,4),(15.1888611523549,15.6834340444711,15.7079632679489),
 .UNSPECIFIED.);
#619=B_SPLINE_CURVE_WITH_KNOTS('',3,(#31812,#31813,#31814,#31815,#31816,
#31817,#31818,#31819,#31820,#31821),.UNSPECIFIED.,.F.,.F.,(4,1,1,1,1,1,
1,4),(13.0854727299533,13.1367272593894,13.6313001515056,14.1258730436219,
14.6204459357381,15.1150188278544,15.6095917199706,15.7079632679489),
 .UNSPECIFIED.);
#620=B_SPLINE_CURVE_WITH_KNOTS('',3,(#31823,#31824,#31825,#31826,#31827,
#31828,#31829,#31830,#31831,#31832,#31833,#31834,#31835,#31836,#31837,#31838),
 .UNSPECIFIED.,.F.,.F.,(4,1,1,1,1,1,1,1,1,1,1,1,1,4),(15.7079632679489,
16.1041646120869,16.5987375042031,17.0933103963194,17.5878832884356,18.0824561805519,
18.5770290726681,19.0716019647843,19.5661748569006,20.0607477490168,20.5553206411331,
21.0498935332493,21.5444664253656,21.9911485751285),.UNSPECIFIED.);
#621=B_SPLINE_CURVE_WITH_KNOTS('',3,(#31839,#31840,#31841,#31842,#31843,
#31844,#31845,#31846,#31847,#31848,#31849,#31850,#31851,#31852,#31853,#31854),
 .UNSPECIFIED.,.F.,.F.,(4,1,1,1,1,1,1,1,1,1,1,1,1,4),(15.7079632679489,
16.1780069365874,16.6725798287036,17.1671527208199,17.6617256129361,18.1562985050523,
18.6508713971686,19.1454442892848,19.6400171814011,20.1345900735173,20.6291629656336,
21.1237358577498,21.6183087498661,21.9911485751285),.UNSPECIFIED.);
#622=B_SPLINE_CURVE_WITH_KNOTS('',3,(#32315,#32316,#32317,#32318,#32319,
#32320,#32321,#32322,#32323,#32324,#32325,#32326,#32327,#32328,#32329,#32330,
#32331,#32332,#32333,#32334,#32335,#32336,#32337,#32338,#32339,#32340,#32341,
#32342,#32343,#32344,#32345),.UNSPECIFIED.,.F.,.F.,(4,3,3,3,3,3,3,3,3,3,
4),(0.,0.0822466706468383,0.162608105240606,0.216579893838171,0.23924274204394,
0.301838371937517,0.36076250940623,0.388067588559334,0.409537377502954,
0.476290104322315,0.53753492181237),.UNSPECIFIED.);
#623=B_SPLINE_CURVE_WITH_KNOTS('',3,(#32346,#32347,#32348,#32349,#32350,
#32351,#32352,#32353,#32354,#32355,#32356,#32357,#32358,#32359,#32360,#32361,
#32362,#32363,#32364,#32365,#32366,#32367,#32368,#32369,#32370,#32371,#32372,
#32373),.UNSPECIFIED.,.F.,.F.,(4,3,3,3,3,3,3,3,3,4),(0.,0.0665230127441691,
0.13429495842692,0.176258819244205,0.195926107024299,0.263526952009386,
0.33682854572103,0.365338415901403,0.449700157257057,0.534061898612711),
 .UNSPECIFIED.);
#624=B_SPLINE_CURVE_WITH_KNOTS('',3,(#32374,#32375,#32376,#32377,#32378,
#32379,#32380,#32381,#32382,#32383,#32384,#32385,#32386,#32387,#32388,#32389,
#32390,#32391,#32392,#32393,#32394,#32395,#32396,#32397,#32398,#32399,#32400,
#32401,#32402,#32403,#32404,#32405,#32406,#32407,#32408,#32409,#32410,#32411,
#32412,#32413),.UNSPECIFIED.,.F.,.F.,(4,3,3,3,3,3,3,3,3,3,3,3,3,4),(-53.8258642502287,
-53.4138723485545,-52.9192994564383,-52.424726564322,-51.9301536722058,
-51.4355807800895,-50.9410078879733,-50.446434995857,-49.9518621037408,
-49.4572892116245,-48.9627163195083,-48.4681434273921,-47.9735705352758,
-47.5426789430491),.UNSPECIFIED.);
#625=B_SPLINE_CURVE_WITH_KNOTS('',3,(#32875,#32876,#32877,#32878,#32879,
#32880,#32881,#32882,#32883,#32884,#32885,#32886,#32887,#32888,#32889,#32890,
#32891,#32892,#32893,#32894,#32895,#32896,#32897,#32898,#32899,#32900,#32901,
#32902),.UNSPECIFIED.,.F.,.F.,(4,3,3,3,3,3,3,3,3,4),(0.,0.0665230199567328,
0.134294967830964,0.176258831509978,0.195926124443112,0.263526952009376,
0.336828549458816,0.365338416771381,0.449700157692121,0.534061898612861),
 .UNSPECIFIED.);
#626=B_SPLINE_CURVE_WITH_KNOTS('',3,(#32903,#32904,#32905,#32906,#32907,
#32908,#32909,#32910,#32911,#32912,#32913,#32914,#32915,#32916,#32917,#32918,
#32919,#32920,#32921,#32922,#32923,#32924,#32925,#32926,#32927,#32928,#32929,
#32930,#32931,#32932,#32933),.UNSPECIFIED.,.F.,.F.,(4,3,3,3,3,3,3,3,3,3,
4),(50.7845845730308,50.9410078879733,51.4355807800895,51.9301536722058,
52.424726564322,52.9192994564383,53.4138723485545,53.9084452406708,54.403018132787,
54.8975910249033,55.3921639170195),.UNSPECIFIED.);
#627=B_SPLINE_CURVE_WITH_KNOTS('',3,(#32934,#32935,#32936,#32937,#32938,
#32939,#32940,#32941,#32942,#32943,#32944,#32945,#32946,#32947,#32948,#32949,
#32950,#32951,#32952,#32953,#32954,#32955,#32956,#32957,#32958,#32959,#32960,
#32961,#32962,#32963,#32964),.UNSPECIFIED.,.F.,.F.,(4,3,3,3,3,3,3,3,3,3,
4),(0.,0.0822466663612967,0.162608100396307,0.216579890867136,0.239242742625966,
0.301838371937549,0.360762509406336,0.388067584071394,0.409537375230468,
0.476290092032249,0.537534921812695),.UNSPECIFIED.);
#1031=SHAPE_REPRESENTATION_RELATIONSHIP('SRR','None',#43847,#1091);
#1091=ADVANCED_BREP_SHAPE_REPRESENTATION('',(#1237),#43507);
#1166=STYLED_ITEM('',(#44209),#1237);
#1237=MANIFOLD_SOLID_BREP('Body1',#18607);
#1553=FACE_BOUND('',#4308,.T.);
#1554=FACE_BOUND('',#4309,.T.);
#1555=FACE_BOUND('',#4310,.T.);
#1556=FACE_BOUND('',#4311,.T.);
#1557=FACE_BOUND('',#4317,.T.);
#1558=FACE_BOUND('',#4318,.T.);
#1559=FACE_BOUND('',#4319,.T.);
#1560=FACE_BOUND('',#4320,.T.);
#1561=FACE_BOUND('',#4325,.T.);
#2083=PLANE('',#20715);
#2084=PLANE('',#20727);
#2085=PLANE('',#20728);
#2086=PLANE('',#20735);
#2933=FACE_OUTER_BOUND('',#4286,.T.);
#2934=FACE_OUTER_BOUND('',#4287,.T.);
#2935=FACE_OUTER_BOUND('',#4288,.T.);
#2936=FACE_OUTER_BOUND('',#4289,.T.);
#2937=FACE_OUTER_BOUND('',#4290,.T.);
#2938=FACE_OUTER_BOUND('',#4291,.T.);
#2939=FACE_OUTER_BOUND('',#4292,.T.);
#2940=FACE_OUTER_BOUND('',#4293,.T.);
#2941=FACE_OUTER_BOUND('',#4294,.T.);
#2942=FACE_OUTER_BOUND('',#4295,.T.);
#2943=FACE_OUTER_BOUND('',#4296,.T.);
#2944=FACE_OUTER_BOUND('',#4297,.T.);
#2945=FACE_OUTER_BOUND('',#4298,.T.);
#2946=FACE_OUTER_BOUND('',#4299,.T.);
#2947=FACE_OUTER_BOUND('',#4300,.T.);
#2948=FACE_OUTER_BOUND('',#4301,.T.);
#2949=FACE_OUTER_BOUND('',#4302,.T.);
#2950=FACE_OUTER_BOUND('',#4303,.T.);
#2951=FACE_OUTER_BOUND('',#4304,.T.);
#2952=FACE_OUTER_BOUND('',#4305,.T.);
#2953=FACE_OUTER_BOUND('',#4306,.T.);
#2954=FACE_OUTER_BOUND('',#4307,.T.);
#2955=FACE_OUTER_BOUND('',#4312,.T.);
#2956=FACE_OUTER_BOUND('',#4313,.T.);
#2957=FACE_OUTER_BOUND('',#4314,.T.);
#2958=FACE_OUTER_BOUND('',#4315,.T.);
#2959=FACE_OUTER_BOUND('',#4316,.T.);
#2960=FACE_OUTER_BOUND('',#4321,.T.);
#2961=FACE_OUTER_BOUND('',#4322,.T.);
#2962=FACE_OUTER_BOUND('',#4323,.T.);
#2963=FACE_OUTER_BOUND('',#4324,.T.);
#4286=EDGE_LOOP('',(#15675,#15676,#15677,#15678));
#4287=EDGE_LOOP('',(#15679,#15680,#15681,#15682));
#4288=EDGE_LOOP('',(#15683,#15684,#15685,#15686));
#4289=EDGE_LOOP('',(#15687,#15688,#15689,#15690));
#4290=EDGE_LOOP('',(#15691,#15692,#15693,#15694));
#4291=EDGE_LOOP('',(#15695,#15696,#15697,#15698));
#4292=EDGE_LOOP('',(#15699,#15700,#15701,#15702));
#4293=EDGE_LOOP('',(#15703,#15704,#15705,#15706));
#4294=EDGE_LOOP('',(#15707,#15708,#15709));
#4295=EDGE_LOOP('',(#15710,#15711,#15712,#15713));
#4296=EDGE_LOOP('',(#15714,#15715,#15716,#15717));
#4297=EDGE_LOOP('',(#15718,#15719,#15720,#15721));
#4298=EDGE_LOOP('',(#15722,#15723,#15724,#15725));
#4299=EDGE_LOOP('',(#15726,#15727,#15728,#15729));
#4300=EDGE_LOOP('',(#15730,#15731,#15732,#15733));
#4301=EDGE_LOOP('',(#15734,#15735,#15736,#15737));
#4302=EDGE_LOOP('',(#15738,#15739,#15740,#15741));
#4303=EDGE_LOOP('',(#15742,#15743,#15744,#15745));
#4304=EDGE_LOOP('',(#15746,#15747,#15748,#15749));
#4305=EDGE_LOOP('',(#15750,#15751,#15752,#15753,#15754,#15755,#15756,#15757,
#15758,#15759,#15760,#15761,#15762,#15763,#15764,#15765,#15766,#15767,#15768,
#15769,#15770,#15771));
#4306=EDGE_LOOP('',(#15772,#15773,#15774,#15775,#15776,#15777,#15778,#15779,
#15780,#15781,#15782,#15783,#15784,#15785,#15786,#15787,#15788,#15789,#15790,
#15791,#15792));
#4307=EDGE_LOOP('',(#15793,#15794));
#4308=EDGE_LOOP('',(#15795,#15796,#15797,#15798,#15799));
#4309=EDGE_LOOP('',(#15800));
#4310=EDGE_LOOP('',(#15801));
#4311=EDGE_LOOP('',(#15802));
#4312=EDGE_LOOP('',(#15803,#15804,#15805,#15806));
#4313=EDGE_LOOP('',(#15807,#15808,#15809,#15810));
#4314=EDGE_LOOP('',(#15811,#15812,#15813,#15814));
#4315=EDGE_LOOP('',(#15815,#15816,#15817,#15818));
#4316=EDGE_LOOP('',(#15819,#15820));
#4317=EDGE_LOOP('',(#15821));
#4318=EDGE_LOOP('',(#15822));
#4319=EDGE_LOOP('',(#15823));
#4320=EDGE_LOOP('',(#15824));
#4321=EDGE_LOOP('',(#15825,#15826,#15827,#15828));
#4322=EDGE_LOOP('',(#15829,#15830,#15831,#15832,#15833));
#4323=EDGE_LOOP('',(#15834,#15835,#15836,#15837));
#4324=EDGE_LOOP('',(#15838));
#4325=EDGE_LOOP('',(#15839,#15840,#15841,#15842));
#5724=LINE('',#30809,#7156);
#5725=LINE('',#30881,#7157);
#5726=LINE('',#30968,#7158);
#5727=LINE('',#31058,#7159);
#5728=LINE('',#31145,#7160);
#5729=LINE('',#31235,#7161);
#5730=LINE('',#31322,#7162);
#5731=LINE('',#31409,#7163);
#5732=LINE('',#31499,#7164);
#5733=LINE('',#31515,#7165);
#5734=LINE('',#31541,#7166);
#5735=LINE('',#31578,#7167);
#5736=LINE('',#31615,#7168);
#5737=LINE('',#31653,#7169);
#5738=LINE('',#31690,#7170);
#5739=LINE('',#31727,#7171);
#5740=LINE('',#31765,#7172);
#5741=LINE('',#31803,#7173);
#5742=LINE('',#32968,#7174);
#5743=LINE('',#32980,#7175);
#5744=LINE('',#32984,#7176);
#5745=LINE('',#32988,#7177);
#5746=LINE('',#32992,#7178);
#5747=LINE('',#32993,#7179);
#5748=LINE('',#32994,#7180);
#5749=LINE('',#33003,#7181);
#7156=VECTOR('',#25132,0.45);
#7157=VECTOR('',#25137,0.45);
#7158=VECTOR('',#25140,0.45);
#7159=VECTOR('',#25143,0.45);
#7160=VECTOR('',#25146,0.45);
#7161=VECTOR('',#25149,0.45);
#7162=VECTOR('',#25152,0.45);
#7163=VECTOR('',#25155,0.45);
#7164=VECTOR('',#25158,0.45);
#7165=VECTOR('',#25163,0.625);
#7166=VECTOR('',#25168,0.625);
#7167=VECTOR('',#25171,0.625);
#7168=VECTOR('',#25174,0.625);
#7169=VECTOR('',#25177,0.625);
#7170=VECTOR('',#25180,0.625);
#7171=VECTOR('',#25183,0.625);
#7172=VECTOR('',#25186,0.625);
#7173=VECTOR('',#25189,0.625);
#7174=VECTOR('',#25196,1.);
#7175=VECTOR('',#25211,0.225);
#7176=VECTOR('',#25216,0.225);
#7177=VECTOR('',#25221,0.225);
#7178=VECTOR('',#25224,1.);
#7179=VECTOR('',#25225,1.);
#7180=VECTOR('',#25226,1.);
#7181=VECTOR('',#25239,1.1);
#8047=CIRCLE('',#20693,0.457875);
#8048=CIRCLE('',#20702,0.457875);
#8049=CIRCLE('',#20704,0.625);
#8050=CIRCLE('',#20713,0.625);
#8051=CIRCLE('',#20716,1.9);
#8052=CIRCLE('',#20717,0.457875);
#8053=CIRCLE('',#20718,0.225);
#8054=CIRCLE('',#20719,0.225);
#8055=CIRCLE('',#20720,0.225);
#8056=CIRCLE('',#20722,0.225);
#8057=CIRCLE('',#20724,0.225);
#8058=CIRCLE('',#20726,0.225);
#8059=CIRCLE('',#20729,1.9);
#8060=CIRCLE('',#20730,1.1);
#8061=CIRCLE('',#20734,1.1);
#9300=VERTEX_POINT('',#30807);
#9301=VERTEX_POINT('',#30808);
#9302=VERTEX_POINT('',#30810);
#9303=VERTEX_POINT('',#30836);
#9304=VERTEX_POINT('',#30879);
#9305=VERTEX_POINT('',#30880);
#9306=VERTEX_POINT('',#30966);
#9307=VERTEX_POINT('',#30967);
#9308=VERTEX_POINT('',#31056);
#9309=VERTEX_POINT('',#31057);
#9310=VERTEX_POINT('',#31143);
#9311=VERTEX_POINT('',#31144);
#9312=VERTEX_POINT('',#31233);
#9313=VERTEX_POINT('',#31234);
#9314=VERTEX_POINT('',#31320);
#9315=VERTEX_POINT('',#31321);
#9316=VERTEX_POINT('',#31407);
#9317=VERTEX_POINT('',#31408);
#9318=VERTEX_POINT('',#31497);
#9319=VERTEX_POINT('',#31498);
#9320=VERTEX_POINT('',#31500);
#9321=VERTEX_POINT('',#31513);
#9322=VERTEX_POINT('',#31514);
#9323=VERTEX_POINT('',#31516);
#9324=VERTEX_POINT('',#31524);
#9325=VERTEX_POINT('',#31539);
#9326=VERTEX_POINT('',#31540);
#9327=VERTEX_POINT('',#31576);
#9328=VERTEX_POINT('',#31577);
#9329=VERTEX_POINT('',#31613);
#9330=VERTEX_POINT('',#31614);
#9331=VERTEX_POINT('',#31651);
#9332=VERTEX_POINT('',#31652);
#9333=VERTEX_POINT('',#31688);
#9334=VERTEX_POINT('',#31689);
#9335=VERTEX_POINT('',#31725);
#9336=VERTEX_POINT('',#31726);
#9337=VERTEX_POINT('',#31763);
#9338=VERTEX_POINT('',#31764);
#9339=VERTEX_POINT('',#31801);
#9340=VERTEX_POINT('',#31802);
#9341=VERTEX_POINT('',#31804);
#9342=VERTEX_POINT('',#31810);
#9343=VERTEX_POINT('',#32874);
#9344=VERTEX_POINT('',#32966);
#9345=VERTEX_POINT('',#32967);
#9346=VERTEX_POINT('',#32971);
#9347=VERTEX_POINT('',#32973);
#9348=VERTEX_POINT('',#32975);
#9349=VERTEX_POINT('',#32978);
#9350=VERTEX_POINT('',#32982);
#9351=VERTEX_POINT('',#32986);
#9352=VERTEX_POINT('',#32990);
#9353=VERTEX_POINT('',#32991);
#9354=VERTEX_POINT('',#32997);
#9355=VERTEX_POINT('',#33002);
#11502=EDGE_CURVE('',#9300,#9301,#5724,.T.);
#11503=EDGE_CURVE('',#9301,#9302,#585,.T.);
#11504=EDGE_CURVE('',#9302,#9303,#8047,.F.);
#11505=EDGE_CURVE('',#9303,#9300,#586,.T.);
#11506=EDGE_CURVE('',#9304,#9305,#5725,.T.);
#11507=EDGE_CURVE('',#9305,#9301,#587,.T.);
#11508=EDGE_CURVE('',#9300,#9304,#588,.T.);
#11509=EDGE_CURVE('',#9306,#9307,#5726,.T.);
#11510=EDGE_CURVE('',#9307,#9305,#589,.T.);
#11511=EDGE_CURVE('',#9304,#9306,#590,.T.);
#11512=EDGE_CURVE('',#9308,#9309,#5727,.T.);
#11513=EDGE_CURVE('',#9309,#9307,#591,.T.);
#11514=EDGE_CURVE('',#9306,#9308,#592,.T.);
#11515=EDGE_CURVE('',#9310,#9311,#5728,.T.);
#11516=EDGE_CURVE('',#9311,#9309,#593,.T.);
#11517=EDGE_CURVE('',#9308,#9310,#594,.T.);
#11518=EDGE_CURVE('',#9312,#9313,#5729,.T.);
#11519=EDGE_CURVE('',#9313,#9311,#595,.T.);
#11520=EDGE_CURVE('',#9310,#9312,#596,.T.);
#11521=EDGE_CURVE('',#9314,#9315,#5730,.T.);
#11522=EDGE_CURVE('',#9315,#9313,#597,.T.);
#11523=EDGE_CURVE('',#9312,#9314,#598,.T.);
#11524=EDGE_CURVE('',#9316,#9317,#5731,.T.);
#11525=EDGE_CURVE('',#9317,#9315,#599,.T.);
#11526=EDGE_CURVE('',#9314,#9316,#600,.T.);
#11527=EDGE_CURVE('',#9318,#9319,#5732,.T.);
#11528=EDGE_CURVE('',#9320,#9318,#8048,.F.);
#11529=EDGE_CURVE('',#9320,#9319,#601,.T.);
#11530=EDGE_CURVE('',#9321,#9322,#5733,.T.);
#11531=EDGE_CURVE('',#9322,#9323,#602,.T.);
#11532=EDGE_CURVE('',#9324,#9323,#8049,.T.);
#11533=EDGE_CURVE('',#9321,#9324,#603,.T.);
#11534=EDGE_CURVE('',#9325,#9326,#5734,.T.);
#11535=EDGE_CURVE('',#9326,#9322,#604,.T.);
#11536=EDGE_CURVE('',#9325,#9321,#605,.T.);
#11537=EDGE_CURVE('',#9327,#9328,#5735,.T.);
#11538=EDGE_CURVE('',#9328,#9326,#606,.T.);
#11539=EDGE_CURVE('',#9327,#9325,#607,.T.);
#11540=EDGE_CURVE('',#9329,#9330,#5736,.T.);
#11541=EDGE_CURVE('',#9330,#9328,#608,.T.);
#11542=EDGE_CURVE('',#9329,#9327,#609,.T.);
#11543=EDGE_CURVE('',#9331,#9332,#5737,.T.);
#11544=EDGE_CURVE('',#9332,#9330,#610,.T.);
#11545=EDGE_CURVE('',#9331,#9329,#611,.T.);
#11546=EDGE_CURVE('',#9333,#9334,#5738,.T.);
#11547=EDGE_CURVE('',#9334,#9332,#612,.T.);
#11548=EDGE_CURVE('',#9333,#9331,#613,.T.);
#11549=EDGE_CURVE('',#9335,#9336,#5739,.T.);
#11550=EDGE_CURVE('',#9336,#9334,#614,.T.);
#11551=EDGE_CURVE('',#9335,#9333,#615,.T.);
#11552=EDGE_CURVE('',#9337,#9338,#5740,.T.);
#11553=EDGE_CURVE('',#9338,#9336,#616,.T.);
#11554=EDGE_CURVE('',#9337,#9335,#617,.T.);
#11555=EDGE_CURVE('',#9339,#9340,#5741,.T.);
#11556=EDGE_CURVE('',#9341,#9339,#618,.T.);
#11557=EDGE_CURVE('',#9342,#9341,#8050,.T.);
#11558=EDGE_CURVE('',#9342,#9340,#619,.T.);
#11559=EDGE_CURVE('',#9340,#9338,#620,.T.);
#11560=EDGE_CURVE('',#9339,#9337,#621,.T.);
#11561=EDGE_CURVE('',#9323,#9320,#622,.T.);
#11562=EDGE_CURVE('',#9302,#9342,#623,.T.);
#11563=EDGE_CURVE('',#9319,#9317,#624,.T.);
#11564=EDGE_CURVE('',#9343,#9324,#625,.T.);
#11565=EDGE_CURVE('',#9316,#9343,#626,.T.);
#11566=EDGE_CURVE('',#9341,#9303,#627,.T.);
#11567=EDGE_CURVE('',#9344,#9345,#5742,.T.);
#11568=EDGE_CURVE('',#9345,#9344,#8051,.T.);
#11569=EDGE_CURVE('',#9318,#9343,#8052,.F.);
#11570=EDGE_CURVE('',#9346,#9346,#8053,.T.);
#11571=EDGE_CURVE('',#9347,#9347,#8054,.T.);
#11572=EDGE_CURVE('',#9348,#9348,#8055,.T.);
#11573=EDGE_CURVE('',#9349,#9349,#8056,.T.);
#11574=EDGE_CURVE('',#9349,#9348,#5743,.T.);
#11575=EDGE_CURVE('',#9350,#9350,#8057,.T.);
#11576=EDGE_CURVE('',#9350,#9347,#5744,.T.);
#11577=EDGE_CURVE('',#9351,#9351,#8058,.T.);
#11578=EDGE_CURVE('',#9351,#9346,#5745,.T.);
#11579=EDGE_CURVE('',#9352,#9353,#5746,.T.);
#11580=EDGE_CURVE('',#9345,#9352,#5747,.T.);
#11581=EDGE_CURVE('',#9353,#9344,#5748,.T.);
#11582=EDGE_CURVE('',#9352,#9353,#8059,.T.);
#11583=EDGE_CURVE('',#9354,#9354,#8060,.T.);
#11584=EDGE_CURVE('',#9354,#9355,#5749,.T.);
#11585=EDGE_CURVE('',#9355,#9355,#8061,.T.);
#15675=ORIENTED_EDGE('',*,*,#11502,.T.);
#15676=ORIENTED_EDGE('',*,*,#11503,.T.);
#15677=ORIENTED_EDGE('',*,*,#11504,.T.);
#15678=ORIENTED_EDGE('',*,*,#11505,.T.);
#15679=ORIENTED_EDGE('',*,*,#11506,.T.);
#15680=ORIENTED_EDGE('',*,*,#11507,.T.);
#15681=ORIENTED_EDGE('',*,*,#11502,.F.);
#15682=ORIENTED_EDGE('',*,*,#11508,.T.);
#15683=ORIENTED_EDGE('',*,*,#11509,.T.);
#15684=ORIENTED_EDGE('',*,*,#11510,.T.);
#15685=ORIENTED_EDGE('',*,*,#11506,.F.);
#15686=ORIENTED_EDGE('',*,*,#11511,.T.);
#15687=ORIENTED_EDGE('',*,*,#11512,.T.);
#15688=ORIENTED_EDGE('',*,*,#11513,.T.);
#15689=ORIENTED_EDGE('',*,*,#11509,.F.);
#15690=ORIENTED_EDGE('',*,*,#11514,.T.);
#15691=ORIENTED_EDGE('',*,*,#11515,.T.);
#15692=ORIENTED_EDGE('',*,*,#11516,.T.);
#15693=ORIENTED_EDGE('',*,*,#11512,.F.);
#15694=ORIENTED_EDGE('',*,*,#11517,.T.);
#15695=ORIENTED_EDGE('',*,*,#11518,.T.);
#15696=ORIENTED_EDGE('',*,*,#11519,.T.);
#15697=ORIENTED_EDGE('',*,*,#11515,.F.);
#15698=ORIENTED_EDGE('',*,*,#11520,.T.);
#15699=ORIENTED_EDGE('',*,*,#11521,.T.);
#15700=ORIENTED_EDGE('',*,*,#11522,.T.);
#15701=ORIENTED_EDGE('',*,*,#11518,.F.);
#15702=ORIENTED_EDGE('',*,*,#11523,.T.);
#15703=ORIENTED_EDGE('',*,*,#11524,.T.);
#15704=ORIENTED_EDGE('',*,*,#11525,.T.);
#15705=ORIENTED_EDGE('',*,*,#11521,.F.);
#15706=ORIENTED_EDGE('',*,*,#11526,.T.);
#15707=ORIENTED_EDGE('',*,*,#11527,.F.);
#15708=ORIENTED_EDGE('',*,*,#11528,.F.);
#15709=ORIENTED_EDGE('',*,*,#11529,.T.);
#15710=ORIENTED_EDGE('',*,*,#11530,.T.);
#15711=ORIENTED_EDGE('',*,*,#11531,.T.);
#15712=ORIENTED_EDGE('',*,*,#11532,.F.);
#15713=ORIENTED_EDGE('',*,*,#11533,.F.);
#15714=ORIENTED_EDGE('',*,*,#11534,.T.);
#15715=ORIENTED_EDGE('',*,*,#11535,.T.);
#15716=ORIENTED_EDGE('',*,*,#11530,.F.);
#15717=ORIENTED_EDGE('',*,*,#11536,.F.);
#15718=ORIENTED_EDGE('',*,*,#11537,.T.);
#15719=ORIENTED_EDGE('',*,*,#11538,.T.);
#15720=ORIENTED_EDGE('',*,*,#11534,.F.);
#15721=ORIENTED_EDGE('',*,*,#11539,.F.);
#15722=ORIENTED_EDGE('',*,*,#11540,.T.);
#15723=ORIENTED_EDGE('',*,*,#11541,.T.);
#15724=ORIENTED_EDGE('',*,*,#11537,.F.);
#15725=ORIENTED_EDGE('',*,*,#11542,.F.);
#15726=ORIENTED_EDGE('',*,*,#11543,.T.);
#15727=ORIENTED_EDGE('',*,*,#11544,.T.);
#15728=ORIENTED_EDGE('',*,*,#11540,.F.);
#15729=ORIENTED_EDGE('',*,*,#11545,.F.);
#15730=ORIENTED_EDGE('',*,*,#11546,.T.);
#15731=ORIENTED_EDGE('',*,*,#11547,.T.);
#15732=ORIENTED_EDGE('',*,*,#11543,.F.);
#15733=ORIENTED_EDGE('',*,*,#11548,.F.);
#15734=ORIENTED_EDGE('',*,*,#11549,.T.);
#15735=ORIENTED_EDGE('',*,*,#11550,.T.);
#15736=ORIENTED_EDGE('',*,*,#11546,.F.);
#15737=ORIENTED_EDGE('',*,*,#11551,.F.);
#15738=ORIENTED_EDGE('',*,*,#11552,.T.);
#15739=ORIENTED_EDGE('',*,*,#11553,.T.);
#15740=ORIENTED_EDGE('',*,*,#11549,.F.);
#15741=ORIENTED_EDGE('',*,*,#11554,.F.);
#15742=ORIENTED_EDGE('',*,*,#11555,.F.);
#15743=ORIENTED_EDGE('',*,*,#11556,.F.);
#15744=ORIENTED_EDGE('',*,*,#11557,.F.);
#15745=ORIENTED_EDGE('',*,*,#11558,.T.);
#15746=ORIENTED_EDGE('',*,*,#11555,.T.);
#15747=ORIENTED_EDGE('',*,*,#11559,.T.);
#15748=ORIENTED_EDGE('',*,*,#11552,.F.);
#15749=ORIENTED_EDGE('',*,*,#11560,.F.);
#15750=ORIENTED_EDGE('',*,*,#11561,.F.);
#15751=ORIENTED_EDGE('',*,*,#11531,.F.);
#15752=ORIENTED_EDGE('',*,*,#11535,.F.);
#15753=ORIENTED_EDGE('',*,*,#11538,.F.);
#15754=ORIENTED_EDGE('',*,*,#11541,.F.);
#15755=ORIENTED_EDGE('',*,*,#11544,.F.);
#15756=ORIENTED_EDGE('',*,*,#11547,.F.);
#15757=ORIENTED_EDGE('',*,*,#11550,.F.);
#15758=ORIENTED_EDGE('',*,*,#11553,.F.);
#15759=ORIENTED_EDGE('',*,*,#11559,.F.);
#15760=ORIENTED_EDGE('',*,*,#11558,.F.);
#15761=ORIENTED_EDGE('',*,*,#11562,.F.);
#15762=ORIENTED_EDGE('',*,*,#11503,.F.);
#15763=ORIENTED_EDGE('',*,*,#11507,.F.);
#15764=ORIENTED_EDGE('',*,*,#11510,.F.);
#15765=ORIENTED_EDGE('',*,*,#11513,.F.);
#15766=ORIENTED_EDGE('',*,*,#11516,.F.);
#15767=ORIENTED_EDGE('',*,*,#11519,.F.);
#15768=ORIENTED_EDGE('',*,*,#11522,.F.);
#15769=ORIENTED_EDGE('',*,*,#11525,.F.);
#15770=ORIENTED_EDGE('',*,*,#11563,.F.);
#15771=ORIENTED_EDGE('',*,*,#11529,.F.);
#15772=ORIENTED_EDGE('',*,*,#11564,.F.);
#15773=ORIENTED_EDGE('',*,*,#11565,.F.);
#15774=ORIENTED_EDGE('',*,*,#11526,.F.);
#15775=ORIENTED_EDGE('',*,*,#11523,.F.);
#15776=ORIENTED_EDGE('',*,*,#11520,.F.);
#15777=ORIENTED_EDGE('',*,*,#11517,.F.);
#15778=ORIENTED_EDGE('',*,*,#11514,.F.);
#15779=ORIENTED_EDGE('',*,*,#11511,.F.);
#15780=ORIENTED_EDGE('',*,*,#11508,.F.);
#15781=ORIENTED_EDGE('',*,*,#11505,.F.);
#15782=ORIENTED_EDGE('',*,*,#11566,.F.);
#15783=ORIENTED_EDGE('',*,*,#11556,.T.);
#15784=ORIENTED_EDGE('',*,*,#11560,.T.);
#15785=ORIENTED_EDGE('',*,*,#11554,.T.);
#15786=ORIENTED_EDGE('',*,*,#11551,.T.);
#15787=ORIENTED_EDGE('',*,*,#11548,.T.);
#15788=ORIENTED_EDGE('',*,*,#11545,.T.);
#15789=ORIENTED_EDGE('',*,*,#11542,.T.);
#15790=ORIENTED_EDGE('',*,*,#11539,.T.);
#15791=ORIENTED_EDGE('',*,*,#11536,.T.);
#15792=ORIENTED_EDGE('',*,*,#11533,.T.);
#15793=ORIENTED_EDGE('',*,*,#11567,.T.);
#15794=ORIENTED_EDGE('',*,*,#11568,.T.);
#15795=ORIENTED_EDGE('',*,*,#11564,.T.);
#15796=ORIENTED_EDGE('',*,*,#11532,.T.);
#15797=ORIENTED_EDGE('',*,*,#11561,.T.);
#15798=ORIENTED_EDGE('',*,*,#11528,.T.);
#15799=ORIENTED_EDGE('',*,*,#11569,.T.);
#15800=ORIENTED_EDGE('',*,*,#11570,.T.);
#15801=ORIENTED_EDGE('',*,*,#11571,.T.);
#15802=ORIENTED_EDGE('',*,*,#11572,.T.);
#15803=ORIENTED_EDGE('',*,*,#11573,.F.);
#15804=ORIENTED_EDGE('',*,*,#11574,.T.);
#15805=ORIENTED_EDGE('',*,*,#11572,.F.);
#15806=ORIENTED_EDGE('',*,*,#11574,.F.);
#15807=ORIENTED_EDGE('',*,*,#11575,.F.);
#15808=ORIENTED_EDGE('',*,*,#11576,.T.);
#15809=ORIENTED_EDGE('',*,*,#11571,.F.);
#15810=ORIENTED_EDGE('',*,*,#11576,.F.);
#15811=ORIENTED_EDGE('',*,*,#11577,.F.);
#15812=ORIENTED_EDGE('',*,*,#11578,.T.);
#15813=ORIENTED_EDGE('',*,*,#11570,.F.);
#15814=ORIENTED_EDGE('',*,*,#11578,.F.);
#15815=ORIENTED_EDGE('',*,*,#11579,.F.);
#15816=ORIENTED_EDGE('',*,*,#11580,.F.);
#15817=ORIENTED_EDGE('',*,*,#11567,.F.);
#15818=ORIENTED_EDGE('',*,*,#11581,.F.);
#15819=ORIENTED_EDGE('',*,*,#11579,.T.);
#15820=ORIENTED_EDGE('',*,*,#11582,.F.);
#15821=ORIENTED_EDGE('',*,*,#11573,.T.);
#15822=ORIENTED_EDGE('',*,*,#11575,.T.);
#15823=ORIENTED_EDGE('',*,*,#11577,.T.);
#15824=ORIENTED_EDGE('',*,*,#11583,.T.);
#15825=ORIENTED_EDGE('',*,*,#11581,.T.);
#15826=ORIENTED_EDGE('',*,*,#11568,.F.);
#15827=ORIENTED_EDGE('',*,*,#11580,.T.);
#15828=ORIENTED_EDGE('',*,*,#11582,.T.);
#15829=ORIENTED_EDGE('',*,*,#11527,.T.);
#15830=ORIENTED_EDGE('',*,*,#11563,.T.);
#15831=ORIENTED_EDGE('',*,*,#11524,.F.);
#15832=ORIENTED_EDGE('',*,*,#11565,.T.);
#15833=ORIENTED_EDGE('',*,*,#11569,.F.);
#15834=ORIENTED_EDGE('',*,*,#11583,.F.);
#15835=ORIENTED_EDGE('',*,*,#11584,.T.);
#15836=ORIENTED_EDGE('',*,*,#11585,.T.);
#15837=ORIENTED_EDGE('',*,*,#11584,.F.);
#15838=ORIENTED_EDGE('',*,*,#11585,.F.);
#15839=ORIENTED_EDGE('',*,*,#11566,.T.);
#15840=ORIENTED_EDGE('',*,*,#11504,.F.);
#15841=ORIENTED_EDGE('',*,*,#11562,.T.);
#15842=ORIENTED_EDGE('',*,*,#11557,.T.);
#17314=CYLINDRICAL_SURFACE('',#20692,0.457875);
#17315=CYLINDRICAL_SURFACE('',#20694,0.457875);
#17316=CYLINDRICAL_SURFACE('',#20695,0.457875);
#17317=CYLINDRICAL_SURFACE('',#20696,0.457875);
#17318=CYLINDRICAL_SURFACE('',#20697,0.457875);
#17319=CYLINDRICAL_SURFACE('',#20698,0.457875);
#17320=CYLINDRICAL_SURFACE('',#20699,0.457875);
#17321=CYLINDRICAL_SURFACE('',#20700,0.457875);
#17322=CYLINDRICAL_SURFACE('',#20701,0.457875);
#17323=CYLINDRICAL_SURFACE('',#20703,0.625);
#17324=CYLINDRICAL_SURFACE('',#20705,0.625);
#17325=CYLINDRICAL_SURFACE('',#20706,0.625);
#17326=CYLINDRICAL_SURFACE('',#20707,0.625);
#17327=CYLINDRICAL_SURFACE('',#20708,0.625);
#17328=CYLINDRICAL_SURFACE('',#20709,0.625);
#17329=CYLINDRICAL_SURFACE('',#20710,0.625);
#17330=CYLINDRICAL_SURFACE('',#20711,0.625);
#17331=CYLINDRICAL_SURFACE('',#20712,0.625);
#17332=CYLINDRICAL_SURFACE('',#20714,0.625);
#17333=CYLINDRICAL_SURFACE('',#20721,0.225);
#17334=CYLINDRICAL_SURFACE('',#20723,0.225);
#17335=CYLINDRICAL_SURFACE('',#20725,0.225);
#17336=CYLINDRICAL_SURFACE('',#20731,1.9);
#17337=CYLINDRICAL_SURFACE('',#20732,0.457875);
#17338=CYLINDRICAL_SURFACE('',#20733,1.1);
#18257=ADVANCED_FACE('',(#2933),#17314,.F.);
#18258=ADVANCED_FACE('',(#2934),#17315,.F.);
#18259=ADVANCED_FACE('',(#2935),#17316,.F.);
#18260=ADVANCED_FACE('',(#2936),#17317,.F.);
#18261=ADVANCED_FACE('',(#2937),#17318,.F.);
#18262=ADVANCED_FACE('',(#2938),#17319,.F.);
#18263=ADVANCED_FACE('',(#2939),#17320,.F.);
#18264=ADVANCED_FACE('',(#2940),#17321,.F.);
#18265=ADVANCED_FACE('',(#2941),#17322,.F.);
#18266=ADVANCED_FACE('',(#2942),#17323,.F.);
#18267=ADVANCED_FACE('',(#2943),#17324,.F.);
#18268=ADVANCED_FACE('',(#2944),#17325,.F.);
#18269=ADVANCED_FACE('',(#2945),#17326,.F.);
#18270=ADVANCED_FACE('',(#2946),#17327,.F.);
#18271=ADVANCED_FACE('',(#2947),#17328,.F.);
#18272=ADVANCED_FACE('',(#2948),#17329,.F.);
#18273=ADVANCED_FACE('',(#2949),#17330,.F.);
#18274=ADVANCED_FACE('',(#2950),#17331,.F.);
#18275=ADVANCED_FACE('',(#2951),#17332,.F.);
#18276=ADVANCED_FACE('',(#2952),#11,.F.);
#18277=ADVANCED_FACE('',(#2953),#12,.F.);
#18278=ADVANCED_FACE('',(#2954,#1553,#1554,#1555,#1556),#2083,.T.);
#18279=ADVANCED_FACE('',(#2955),#17333,.F.);
#18280=ADVANCED_FACE('',(#2956),#17334,.F.);
#18281=ADVANCED_FACE('',(#2957),#17335,.F.);
#18282=ADVANCED_FACE('',(#2958),#2084,.F.);
#18283=ADVANCED_FACE('',(#2959,#1557,#1558,#1559,#1560),#2085,.F.);
#18284=ADVANCED_FACE('',(#2960),#17336,.T.);
#18285=ADVANCED_FACE('',(#2961),#17337,.F.);
#18286=ADVANCED_FACE('',(#2962),#17338,.T.);
#18287=ADVANCED_FACE('',(#2963,#1561),#2086,.F.);
#18607=CLOSED_SHELL('',(#18257,#18258,#18259,#18260,#18261,#18262,#18263,
#18264,#18265,#18266,#18267,#18268,#18269,#18270,#18271,#18272,#18273,#18274,
#18275,#18276,#18277,#18278,#18279,#18280,#18281,#18282,#18283,#18284,#18285,
#18286,#18287));
#20691=AXIS2_PLACEMENT_3D('',#30805,#25128,#25129);
#20692=AXIS2_PLACEMENT_3D('',#30806,#25130,#25131);
#20693=AXIS2_PLACEMENT_3D('',#30837,#25133,#25134);
#20694=AXIS2_PLACEMENT_3D('',#30878,#25135,#25136);
#20695=AXIS2_PLACEMENT_3D('',#30965,#25138,#25139);
#20696=AXIS2_PLACEMENT_3D('',#31055,#25141,#25142);
#20697=AXIS2_PLACEMENT_3D('',#31142,#25144,#25145);
#20698=AXIS2_PLACEMENT_3D('',#31232,#25147,#25148);
#20699=AXIS2_PLACEMENT_3D('',#31319,#25150,#25151);
#20700=AXIS2_PLACEMENT_3D('',#31406,#25153,#25154);
#20701=AXIS2_PLACEMENT_3D('',#31496,#25156,#25157);
#20702=AXIS2_PLACEMENT_3D('',#31501,#25159,#25160);
#20703=AXIS2_PLACEMENT_3D('',#31512,#25161,#25162);
#20704=AXIS2_PLACEMENT_3D('',#31525,#25164,#25165);
#20705=AXIS2_PLACEMENT_3D('',#31538,#25166,#25167);
#20706=AXIS2_PLACEMENT_3D('',#31575,#25169,#25170);
#20707=AXIS2_PLACEMENT_3D('',#31612,#25172,#25173);
#20708=AXIS2_PLACEMENT_3D('',#31650,#25175,#25176);
#20709=AXIS2_PLACEMENT_3D('',#31687,#25178,#25179);
#20710=AXIS2_PLACEMENT_3D('',#31724,#25181,#25182);
#20711=AXIS2_PLACEMENT_3D('',#31762,#25184,#25185);
#20712=AXIS2_PLACEMENT_3D('',#31800,#25187,#25188);
#20713=AXIS2_PLACEMENT_3D('',#31811,#25190,#25191);
#20714=AXIS2_PLACEMENT_3D('',#31822,#25192,#25193);
#20715=AXIS2_PLACEMENT_3D('',#32965,#25194,#25195);
#20716=AXIS2_PLACEMENT_3D('',#32969,#25197,#25198);
#20717=AXIS2_PLACEMENT_3D('',#32970,#25199,#25200);
#20718=AXIS2_PLACEMENT_3D('',#32972,#25201,#25202);
#20719=AXIS2_PLACEMENT_3D('',#32974,#25203,#25204);
#20720=AXIS2_PLACEMENT_3D('',#32976,#25205,#25206);
#20721=AXIS2_PLACEMENT_3D('',#32977,#25207,#25208);
#20722=AXIS2_PLACEMENT_3D('',#32979,#25209,#25210);
#20723=AXIS2_PLACEMENT_3D('',#32981,#25212,#25213);
#20724=AXIS2_PLACEMENT_3D('',#32983,#25214,#25215);
#20725=AXIS2_PLACEMENT_3D('',#32985,#25217,#25218);
#20726=AXIS2_PLACEMENT_3D('',#32987,#25219,#25220);
#20727=AXIS2_PLACEMENT_3D('',#32989,#25222,#25223);
#20728=AXIS2_PLACEMENT_3D('',#32995,#25227,#25228);
#20729=AXIS2_PLACEMENT_3D('',#32996,#25229,#25230);
#20730=AXIS2_PLACEMENT_3D('',#32998,#25231,#25232);
#20731=AXIS2_PLACEMENT_3D('',#32999,#25233,#25234);
#20732=AXIS2_PLACEMENT_3D('',#33000,#25235,#25236);
#20733=AXIS2_PLACEMENT_3D('',#33001,#25237,#25238);
#20734=AXIS2_PLACEMENT_3D('',#33004,#25240,#25241);
#20735=AXIS2_PLACEMENT_3D('',#33005,#25242,#25243);
#25128=DIRECTION('axis',(0.,0.,1.));
#25129=DIRECTION('refdir',(1.,0.,0.));
#25130=DIRECTION('center_axis',(1.,0.,0.));
#25131=DIRECTION('ref_axis',(0.,0.207879895528894,-0.978154358490978));
#25132=DIRECTION('',(-1.,0.,0.));
#25133=DIRECTION('center_axis',(1.,0.,0.));
#25134=DIRECTION('ref_axis',(0.,0.,-1.));
#25135=DIRECTION('center_axis',(1.,0.,0.));
#25136=DIRECTION('ref_axis',(0.,0.,-1.));
#25137=DIRECTION('',(-1.,0.,0.));
#25138=DIRECTION('center_axis',(1.,0.,0.));
#25139=DIRECTION('ref_axis',(0.,0.,-1.));
#25140=DIRECTION('',(-1.,0.,0.));
#25141=DIRECTION('center_axis',(1.,0.,0.));
#25142=DIRECTION('ref_axis',(0.,0.,-1.));
#25143=DIRECTION('',(-1.,0.,0.));
#25144=DIRECTION('center_axis',(1.,0.,0.));
#25145=DIRECTION('ref_axis',(0.,0.,-1.));
#25146=DIRECTION('',(-1.,0.,0.));
#25147=DIRECTION('center_axis',(1.,0.,0.));
#25148=DIRECTION('ref_axis',(0.,0.,-1.));
#25149=DIRECTION('',(-1.,0.,0.));
#25150=DIRECTION('center_axis',(1.,0.,0.));
#25151=DIRECTION('ref_axis',(0.,0.,-1.));
#25152=DIRECTION('',(-1.,0.,0.));
#25153=DIRECTION('center_axis',(1.,0.,0.));
#25154=DIRECTION('ref_axis',(0.,0.,-1.));
#25155=DIRECTION('',(-1.,0.,0.));
#25156=DIRECTION('center_axis',(1.,0.,0.));
#25157=DIRECTION('ref_axis',(0.,0.,-1.));
#25158=DIRECTION('',(-1.,0.,0.));
#25159=DIRECTION('center_axis',(1.,0.,0.));
#25160=DIRECTION('ref_axis',(0.,0.,-1.));
#25161=DIRECTION('center_axis',(1.,0.,0.));
#25162=DIRECTION('ref_axis',(0.,2.68771689099506E-14,-1.));
#25163=DIRECTION('',(1.,3.30650148539799E-30,-1.22464679914735E-16));
#25164=DIRECTION('center_axis',(-1.,0.,0.));
#25165=DIRECTION('ref_axis',(0.,2.68771689099506E-14,-1.));
#25166=DIRECTION('center_axis',(1.,0.,0.));
#25167=DIRECTION('ref_axis',(0.,2.68771689099506E-14,-1.));
#25168=DIRECTION('',(1.,3.30650148539799E-30,-1.22464679914735E-16));
#25169=DIRECTION('center_axis',(1.,0.,0.));
#25170=DIRECTION('ref_axis',(0.,2.68771689099506E-14,-1.));
#25171=DIRECTION('',(1.,3.30650148539799E-30,-1.22464679914735E-16));
#25172=DIRECTION('center_axis',(1.,0.,0.));
#25173=DIRECTION('ref_axis',(0.,2.68771689099506E-14,-1.));
#25174=DIRECTION('',(1.,3.30650148539799E-30,-1.22464679914735E-16));
#25175=DIRECTION('center_axis',(1.,0.,0.));
#25176=DIRECTION('ref_axis',(0.,2.68771689099506E-14,-1.));
#25177=DIRECTION('',(1.,3.30650148539799E-30,-1.22464679914735E-16));
#25178=DIRECTION('center_axis',(1.,0.,0.));
#25179=DIRECTION('ref_axis',(0.,2.68771689099506E-14,-1.));
#25180=DIRECTION('',(1.,3.30650148539799E-30,-1.22464679914735E-16));
#25181=DIRECTION('center_axis',(1.,0.,0.));
#25182=DIRECTION('ref_axis',(0.,2.68771689099506E-14,-1.));
#25183=DIRECTION('',(1.,3.30650148539799E-30,-1.22464679914735E-16));
#25184=DIRECTION('center_axis',(1.,0.,0.));
#25185=DIRECTION('ref_axis',(0.,2.68771689099506E-14,-1.));
#25186=DIRECTION('',(1.,3.30650148539799E-30,-1.22464679914735E-16));
#25187=DIRECTION('center_axis',(1.,0.,0.));
#25188=DIRECTION('ref_axis',(0.,2.68771689099506E-14,-1.));
#25189=DIRECTION('',(1.,3.30650148539799E-30,-1.22464679914735E-16));
#25190=DIRECTION('center_axis',(1.,0.,0.));
#25191=DIRECTION('ref_axis',(0.,2.68771689099506E-14,-1.));
#25192=DIRECTION('center_axis',(1.,0.,0.));
#25193=DIRECTION('ref_axis',(0.,2.68771689099506E-14,-1.));
#25194=DIRECTION('center_axis',(1.,0.,0.));
#25195=DIRECTION('ref_axis',(0.,0.,-1.));
#25196=DIRECTION('',(0.,1.,0.));
#25197=DIRECTION('center_axis',(1.,0.,0.));
#25198=DIRECTION('ref_axis',(0.,0.,-1.));
#25199=DIRECTION('center_axis',(1.,0.,0.));
#25200=DIRECTION('ref_axis',(0.,0.,-1.));
#25201=DIRECTION('center_axis',(-1.,0.,0.));
#25202=DIRECTION('ref_axis',(0.,0.,-1.));
#25203=DIRECTION('center_axis',(-1.,0.,0.));
#25204=DIRECTION('ref_axis',(0.,0.,-1.));
#25205=DIRECTION('center_axis',(-1.,0.,0.));
#25206=DIRECTION('ref_axis',(0.,0.,-1.));
#25207=DIRECTION('center_axis',(1.,0.,0.));
#25208=DIRECTION('ref_axis',(0.,0.,-1.));
#25209=DIRECTION('center_axis',(1.,0.,0.));
#25210=DIRECTION('ref_axis',(0.,0.,-1.));
#25211=DIRECTION('',(1.,0.,0.));
#25212=DIRECTION('center_axis',(1.,0.,0.));
#25213=DIRECTION('ref_axis',(0.,0.,-1.));
#25214=DIRECTION('center_axis',(1.,0.,0.));
#25215=DIRECTION('ref_axis',(0.,0.,-1.));
#25216=DIRECTION('',(1.,0.,0.));
#25217=DIRECTION('center_axis',(1.,0.,0.));
#25218=DIRECTION('ref_axis',(0.,0.,-1.));
#25219=DIRECTION('center_axis',(1.,0.,0.));
#25220=DIRECTION('ref_axis',(0.,0.,-1.));
#25221=DIRECTION('',(1.,0.,0.));
#25222=DIRECTION('center_axis',(0.,0.,1.));
#25223=DIRECTION('ref_axis',(0.,-1.,0.));
#25224=DIRECTION('',(0.,-1.,0.));
#25225=DIRECTION('',(-1.,0.,0.));
#25226=DIRECTION('',(1.,0.,0.));
#25227=DIRECTION('center_axis',(1.,0.,0.));
#25228=DIRECTION('ref_axis',(0.,0.,-1.));
#25229=DIRECTION('center_axis',(1.,0.,0.));
#25230=DIRECTION('ref_axis',(0.,0.,-1.));
#25231=DIRECTION('center_axis',(1.,0.,0.));
#25232=DIRECTION('ref_axis',(0.,0.,-1.));
#25233=DIRECTION('center_axis',(1.,0.,0.));
#25234=DIRECTION('ref_axis',(0.,-1.22464679914735E-16,1.));
#25235=DIRECTION('center_axis',(1.,0.,0.));
#25236=DIRECTION('ref_axis',(0.,0.,-1.));
#25237=DIRECTION('center_axis',(1.,0.,0.));
#25238=DIRECTION('ref_axis',(0.,0.,-1.));
#25239=DIRECTION('',(-1.,0.,0.));
#25240=DIRECTION('center_axis',(1.,0.,0.));
#25241=DIRECTION('ref_axis',(0.,0.,-1.));
#25242=DIRECTION('center_axis',(1.,0.,0.));
#25243=DIRECTION('ref_axis',(0.,0.,-1.));
#30805=CARTESIAN_POINT('',(0.,0.,0.));
#30806=CARTESIAN_POINT('Origin',(12.5,0.,4.));
#30807=CARTESIAN_POINT('',(12.7800042915148,-1.13874042544416E-5,4.45787212683272));
#30808=CARTESIAN_POINT('',(12.6699957084852,1.09516003635735E-5,4.45788309353564));
#30809=CARTESIAN_POINT('',(12.5,-5.60735153159594E-17,4.457875));
#30810=CARTESIAN_POINT('',(12.5,-0.186196943290586,3.58169363627331));
#30811=CARTESIAN_POINT('Ctrl Pts',(12.6699957084852,1.09516003635735E-5,
4.45788309353564));
#30812=CARTESIAN_POINT('Ctrl Pts',(12.6684300766731,0.0150239422001319,
4.45789815019349));
#30813=CARTESIAN_POINT('Ctrl Pts',(12.6668644448611,0.0300354905662504,
4.45717403092565));
#30814=CARTESIAN_POINT('Ctrl Pts',(12.6652988130491,0.0449730203321769,
4.45569984746698));
#30815=CARTESIAN_POINT('Ctrl Pts',(12.6574274409991,0.120072959788606,4.44828824124903));
#30816=CARTESIAN_POINT('Ctrl Pts',(12.6495560689492,0.193301947984492,4.42191743369942));
#30817=CARTESIAN_POINT('Ctrl Pts',(12.6416846968992,0.255884660534875,4.37974732787395));
#30818=CARTESIAN_POINT('Ctrl Pts',(12.6338133248492,0.318467373085258,4.33757722204849));
#30819=CARTESIAN_POINT('Ctrl Pts',(12.6259419527993,0.370403809990138,4.27960781794716));
#30820=CARTESIAN_POINT('Ctrl Pts',(12.6180705807493,0.405471379329245,4.2127856577826));
#30821=CARTESIAN_POINT('Ctrl Pts',(12.6101992086994,0.440538948668352,4.14596349761803));
#30822=CARTESIAN_POINT('Ctrl Pts',(12.6023278366494,0.458737650441686,4.07028858139023));
#30823=CARTESIAN_POINT('Ctrl Pts',(12.5944564645995,0.457884906392306,3.99482861029462));
#30824=CARTESIAN_POINT('Ctrl Pts',(12.5865850925495,0.457032162342926,3.91936863919901));
#30825=CARTESIAN_POINT('Ctrl Pts',(12.5787137204996,0.437127972470831,3.84412361323559));
#30826=CARTESIAN_POINT('Ctrl Pts',(12.5708423484496,0.400561475243013,3.77811083326841));
#30827=CARTESIAN_POINT('Ctrl Pts',(12.5629709763996,0.363994978015195,3.71209805330123));
#30828=CARTESIAN_POINT('Ctrl Pts',(12.5550996043497,0.310766173431653,3.6553175193303));
#30829=CARTESIAN_POINT('Ctrl Pts',(12.5472282322997,0.247245050961511,3.61457214242492));
#30830=CARTESIAN_POINT('Ctrl Pts',(12.5393568602498,0.183723928491369,3.57382676551955));
#30831=CARTESIAN_POINT('Ctrl Pts',(12.5314854881998,0.109910488134627,3.54911654567973));
#30832=CARTESIAN_POINT('Ctrl Pts',(12.5236141161499,0.034670519197381,3.5434092666393));
#30833=CARTESIAN_POINT('Ctrl Pts',(12.5157427440999,-0.0405694497398647,
3.53770198759887));
#30834=CARTESIAN_POINT('Ctrl Pts',(12.50787137205,-0.117235947257613,3.55099764935784));
#30835=CARTESIAN_POINT('Ctrl Pts',(12.5,-0.186196943290592,3.58169363627332));
#30836=CARTESIAN_POINT('',(12.5,-0.186217277007329,4.41832740439831));
#30837=CARTESIAN_POINT('Origin',(12.5,0.,4.));
#30838=CARTESIAN_POINT('Ctrl Pts',(12.5,-0.186217277007329,4.41832740439831));
#30839=CARTESIAN_POINT('Ctrl Pts',(12.5008157411716,-0.193365324225124,
4.41515241707318));
#30840=CARTESIAN_POINT('Ctrl Pts',(12.5016314823431,-0.200430783441492,
4.4117927098014));
#30841=CARTESIAN_POINT('Ctrl Pts',(12.5024472235147,-0.207403505574881,
4.40825058102053));
#30842=CARTESIAN_POINT('Ctrl Pts',(12.5103185955646,-0.274685741688951,
4.37407134077235));
#30843=CARTESIAN_POINT('Ctrl Pts',(12.5181899676146,-0.333333232193243,
4.32290684204764));
#30844=CARTESIAN_POINT('Ctrl Pts',(12.5260613396645,-0.376326743005614,
4.26088786252735));
#30845=CARTESIAN_POINT('Ctrl Pts',(12.5339327117145,-0.419320253817985,
4.19886888300706));
#30846=CARTESIAN_POINT('Ctrl Pts',(12.5418040837645,-0.446659784938435,
4.12599542269119));
#30847=CARTESIAN_POINT('Ctrl Pts',(12.5496754558144,-0.455065168373522,
4.05100019606997));
#30848=CARTESIAN_POINT('Ctrl Pts',(12.5575468278644,-0.463470551808608,
3.97600496944875));
#30849=CARTESIAN_POINT('Ctrl Pts',(12.5654181999143,-0.452941787558331,
3.89888797652218));
#30850=CARTESIAN_POINT('Ctrl Pts',(12.5732895719643,-0.424742400952558,
3.82888990513641));
#30851=CARTESIAN_POINT('Ctrl Pts',(12.5811609440142,-0.396543014346786,
3.75889183375065));
#30852=CARTESIAN_POINT('Ctrl Pts',(12.5890323160642,-0.350673005385519,
3.69601268390568));
#30853=CARTESIAN_POINT('Ctrl Pts',(12.5969036881141,-0.292628022669152,
3.64778723809593));
#30854=CARTESIAN_POINT('Ctrl Pts',(12.6047750601641,-0.234583039952784,
3.59956179228618));
#30855=CARTESIAN_POINT('Ctrl Pts',(12.6126464322141,-0.164363083481316,
3.56599005051166));
#30856=CARTESIAN_POINT('Ctrl Pts',(12.620517804264,-0.0903829156297007,
3.55109483330951));
#30857=CARTESIAN_POINT('Ctrl Pts',(12.628389176314,-0.0164027477780855,
3.53619961610736));
#30858=CARTESIAN_POINT('Ctrl Pts',(12.6362605483639,0.0613376314536766,
3.53998092347757));
#30859=CARTESIAN_POINT('Ctrl Pts',(12.6441319204139,0.13352290298843,3.56198566164487));
#30860=CARTESIAN_POINT('Ctrl Pts',(12.6520032924638,0.205708174523184,3.58399039981218));
#30861=CARTESIAN_POINT('Ctrl Pts',(12.6598746645138,0.272338338360929,3.62421856877658));
#30862=CARTESIAN_POINT('Ctrl Pts',(12.6677460365637,0.325429113408527,3.67784968145944));
#30863=CARTESIAN_POINT('Ctrl Pts',(12.6756174086137,0.378519888456125,3.7314807941423));
#30864=CARTESIAN_POINT('Ctrl Pts',(12.6834887806637,0.418071274713577,3.79851485054363));
#30865=CARTESIAN_POINT('Ctrl Pts',(12.6913601527136,0.439343931585728,3.87091926467948));
#30866=CARTESIAN_POINT('Ctrl Pts',(12.6992315247636,0.460616588457879,3.94332367881533));
#30867=CARTESIAN_POINT('Ctrl Pts',(12.7071028968135,0.46361051594473,4.02109845068571));
#30868=CARTESIAN_POINT('Ctrl Pts',(12.7149742688635,0.447966936692366,4.09492394607626));
#30869=CARTESIAN_POINT('Ctrl Pts',(12.7228456409134,0.432323357440003,4.16874944146681));
#30870=CARTESIAN_POINT('Ctrl Pts',(12.7307170129634,0.398042271448426,4.23862566037754));
#30871=CARTESIAN_POINT('Ctrl Pts',(12.7385883850133,0.349231538304918,4.29617944234672));
#30872=CARTESIAN_POINT('Ctrl Pts',(12.7464597570633,0.300420805161409,4.35373322431589));
#30873=CARTESIAN_POINT('Ctrl Pts',(12.7543311291133,0.237080424865968,4.39896456934351));
#30874=CARTESIAN_POINT('Ctrl Pts',(12.7622025011632,0.166800374688878,4.42645347375649));
#30875=CARTESIAN_POINT('Ctrl Pts',(12.7681364312804,0.113818899065861,4.4471763206439));
#30876=CARTESIAN_POINT('Ctrl Pts',(12.7740703613976,0.056893551674301,4.45781599184163));
#30877=CARTESIAN_POINT('Ctrl Pts',(12.7800042915148,-1.13874042544416E-5,
4.45787212683272));
#30878=CARTESIAN_POINT('Origin',(12.5,0.,4.));
#30879=CARTESIAN_POINT('',(13.0800042915148,2.8196954984682E-6,4.45783894202495));
#30880=CARTESIAN_POINT('',(12.9699957084852,-6.90274666573233E-6,4.45790451736119));
#30881=CARTESIAN_POINT('',(12.5,-5.60735153159594E-17,4.457875));
#30882=CARTESIAN_POINT('Ctrl Pts',(12.9699957084852,-6.90274666573233E-6,
4.45790451736119));
#30883=CARTESIAN_POINT('Ctrl Pts',(12.9628865412726,0.0681543496286777,
4.45785453236543));
#30884=CARTESIAN_POINT('Ctrl Pts',(12.95577737406,0.136337475731944,4.44242789501186));
#30885=CARTESIAN_POINT('Ctrl Pts',(12.9486682068475,0.197807532932104,4.41298560914613));
#30886=CARTESIAN_POINT('Ctrl Pts',(12.9407968347975,0.265868063186489,4.38038668734267));
#30887=CARTESIAN_POINT('Ctrl Pts',(12.9329254627476,0.325698883531032,4.33060565060516));
#30888=CARTESIAN_POINT('Ctrl Pts',(12.9250540906976,0.370130557623211,4.26960768492436));
#30889=CARTESIAN_POINT('Ctrl Pts',(12.9171827186476,0.41456223171539,4.20860971924356));
#30890=CARTESIAN_POINT('Ctrl Pts',(12.9093113465977,0.443594759555206,4.13639482461947));
#30891=CARTESIAN_POINT('Ctrl Pts',(12.9014399745477,0.453749217534713,4.06161640217293));
#30892=CARTESIAN_POINT('Ctrl Pts',(12.8935686024978,0.463903675514219,3.9868379797264));
#30893=CARTESIAN_POINT('Ctrl Pts',(12.8856972304478,0.455180063633418,3.90949602945742));
#30894=CARTESIAN_POINT('Ctrl Pts',(12.8778258583979,0.428623718850503,3.83885831972366));
#30895=CARTESIAN_POINT('Ctrl Pts',(12.8699544863479,0.402067374067587,3.7682206099899));
#30896=CARTESIAN_POINT('Ctrl Pts',(12.862083114298,0.357678296382559,3.70428714079136));
#30897=CARTESIAN_POINT('Ctrl Pts',(12.854211742248,0.300775561959983,3.65471896268111));
#30898=CARTESIAN_POINT('Ctrl Pts',(12.846340370198,0.243872827537407,3.60515078457087));
#30899=CARTESIAN_POINT('Ctrl Pts',(12.8384689981481,0.174456436377283,3.56994789754891));
#30900=CARTESIAN_POINT('Ctrl Pts',(12.8305976260981,0.100844448250471,3.55332860992135));
#30901=CARTESIAN_POINT('Ctrl Pts',(12.8227262540482,0.0272324601236582,
3.53670932229378));
#30902=CARTESIAN_POINT('Ctrl Pts',(12.8148548819982,-0.0505751249698428,
3.53867363406062));
#30903=CARTESIAN_POINT('Ctrl Pts',(12.8069835099483,-0.123254740362562,
3.558986165072));
#30904=CARTESIAN_POINT('Ctrl Pts',(12.7991121378983,-0.195934355755281,
3.57929869608338));
#30905=CARTESIAN_POINT('Ctrl Pts',(12.7912407658484,-0.263486001447217,
3.6179594463393));
#30906=CARTESIAN_POINT('Ctrl Pts',(12.7833693937984,-0.317815070570116,
3.67033575613656));
#30907=CARTESIAN_POINT('Ctrl Pts',(12.7754980217484,-0.372144139693014,
3.72271206593382));
#30908=CARTESIAN_POINT('Ctrl Pts',(12.7676266496985,-0.413250632246875,
3.78880393527241));
#30909=CARTESIAN_POINT('Ctrl Pts',(12.7597552776485,-0.43620881068128,3.86069167744737));
#30910=CARTESIAN_POINT('Ctrl Pts',(12.7518839055986,-0.459166989115684,
3.93257941962233));
#30911=CARTESIAN_POINT('Ctrl Pts',(12.7440125335486,-0.463976853430633,
4.01026303463365));
#30912=CARTESIAN_POINT('Ctrl Pts',(12.7361411614987,-0.450062064178823,
4.08443380953254));
#30913=CARTESIAN_POINT('Ctrl Pts',(12.7282697894487,-0.436147274927012,
4.15860458443143));
#30914=CARTESIAN_POINT('Ctrl Pts',(12.7203984173988,-0.403507832108441,
4.22926251921788));
#30915=CARTESIAN_POINT('Ctrl Pts',(12.7125270453488,-0.356054829243877,
4.28794078818664));
#30916=CARTESIAN_POINT('Ctrl Pts',(12.7046556732988,-0.308601826379312,
4.3466190571554));
#30917=CARTESIAN_POINT('Ctrl Pts',(12.6967843012489,-0.246335263468753,
4.39331766030646));
#30918=CARTESIAN_POINT('Ctrl Pts',(12.6889129291989,-0.176716536654988,
4.42244075943884));
#30919=CARTESIAN_POINT('Ctrl Pts',(12.682607188961,-0.120945115332726,4.44577121528397));
#30920=CARTESIAN_POINT('Ctrl Pts',(12.6763014487231,-0.0604553842193124,
4.45782245132557));
#30921=CARTESIAN_POINT('Ctrl Pts',(12.6699957084852,1.09516003635735E-5,
4.45788309353564));
#30922=CARTESIAN_POINT('Ctrl Pts',(12.7800042915148,-1.13874042544416E-5,
4.45787212683272));
#30923=CARTESIAN_POINT('Ctrl Pts',(12.7819417334476,-0.0185909818676029,
4.45789045503738));
#30924=CARTESIAN_POINT('Ctrl Pts',(12.7838791753803,-0.0371684007279871,
4.45678053845584));
#30925=CARTESIAN_POINT('Ctrl Pts',(12.7858166173131,-0.0556056617636943,
4.45452496135198));
#30926=CARTESIAN_POINT('Ctrl Pts',(12.793687989363,-0.130511927980435,4.44536108073615));
#30927=CARTESIAN_POINT('Ctrl Pts',(12.801559361413,-0.203104740355178,4.41728685570614));
#30928=CARTESIAN_POINT('Ctrl Pts',(12.8094307334629,-0.264685413403174,
4.37366637792357));
#30929=CARTESIAN_POINT('Ctrl Pts',(12.8173021055129,-0.32626608645117,4.33004590014099));
#30930=CARTESIAN_POINT('Ctrl Pts',(12.8251734775629,-0.37683462017242,4.27087916960585));
#30931=CARTESIAN_POINT('Ctrl Pts',(12.8330448496128,-0.410331463567461,
4.20325604577686));
#30932=CARTESIAN_POINT('Ctrl Pts',(12.8409162216628,-0.443828306962503,
4.13563292194788));
#30933=CARTESIAN_POINT('Ctrl Pts',(12.8487875937127,-0.460253460031337,
4.05955340482505));
#30934=CARTESIAN_POINT('Ctrl Pts',(12.8566589657627,-0.457638721839564,
3.98413398734005));
#30935=CARTESIAN_POINT('Ctrl Pts',(12.8645303378126,-0.45502398364779,3.90871456985506));
#30936=CARTESIAN_POINT('Ctrl Pts',(12.8724017098626,-0.433369354195409,
3.8339552520079));
#30937=CARTESIAN_POINT('Ctrl Pts',(12.8802730819125,-0.395269674734573,
3.76881432927916));
#30938=CARTESIAN_POINT('Ctrl Pts',(12.8881444539625,-0.357169995273737,
3.70367340655041));
#30939=CARTESIAN_POINT('Ctrl Pts',(12.8960158260125,-0.302625265804445,
3.64815087894007));
#30940=CARTESIAN_POINT('Ctrl Pts',(12.9038871980624,-0.238171498431664,
3.6088999265713));
#30941=CARTESIAN_POINT('Ctrl Pts',(12.9117585701124,-0.173717731058884,
3.56964897420252));
#30942=CARTESIAN_POINT('Ctrl Pts',(12.9196299421623,-0.0993549257826154,
3.5466695970753));
#30943=CARTESIAN_POINT('Ctrl Pts',(12.9275013142123,-0.023993864556795,
3.54271537903906));
#30944=CARTESIAN_POINT('Ctrl Pts',(12.9353726862622,0.0513671966690251,
3.53876116100282));
#30945=CARTESIAN_POINT('Ctrl Pts',(12.9432440583122,0.127726513844396,3.55383210205756));
#30946=CARTESIAN_POINT('Ctrl Pts',(12.9511154303621,0.195934065997641,3.58612227423372));
#30947=CARTESIAN_POINT('Ctrl Pts',(12.9589868024121,0.264141618150887,3.61841244640988));
#30948=CARTESIAN_POINT('Ctrl Pts',(12.9668581744621,0.324197405282005,3.66792184970745));
#30949=CARTESIAN_POINT('Ctrl Pts',(12.974729546512,0.368905033668178,3.72871784755079));
#30950=CARTESIAN_POINT('Ctrl Pts',(12.982600918562,0.41361266205435,3.78951384539413));
#30951=CARTESIAN_POINT('Ctrl Pts',(12.9904722906119,0.442972131695578,3.86159643778324));
#30952=CARTESIAN_POINT('Ctrl Pts',(12.9983436626619,0.453465341949404,3.93632807718928));
#30953=CARTESIAN_POINT('Ctrl Pts',(13.0062150347118,0.46395855220323,4.01105971659532));
#30954=CARTESIAN_POINT('Ctrl Pts',(13.0140864067618,0.455585503069655,4.0884404030183));
#30955=CARTESIAN_POINT('Ctrl Pts',(13.0219577788117,0.429349524305901,4.15919772637108));
#30956=CARTESIAN_POINT('Ctrl Pts',(13.0298291508617,0.403113545542148,4.22995504972387));
#30957=CARTESIAN_POINT('Ctrl Pts',(13.0377005229117,0.359014637148215,4.29408901000646));
#30958=CARTESIAN_POINT('Ctrl Pts',(13.0455718949616,0.302337104315659,4.34391453219887));
#30959=CARTESIAN_POINT('Ctrl Pts',(13.0534432670116,0.245659571483104,4.39374005439127));
#30960=CARTESIAN_POINT('Ctrl Pts',(13.0613146390615,0.176403414211925,4.4292571384935));
#30961=CARTESIAN_POINT('Ctrl Pts',(13.0691860111115,0.102867492605122,4.44620982627979));
#30962=CARTESIAN_POINT('Ctrl Pts',(13.0727921045793,0.0691786509558273,
4.45397632191734));
#30963=CARTESIAN_POINT('Ctrl Pts',(13.076398198047,0.0345915681853763,4.45784650391406));
#30964=CARTESIAN_POINT('Ctrl Pts',(13.0800042915148,2.8196954984682E-6,
4.45783894202495));
#30965=CARTESIAN_POINT('Origin',(12.5,0.,4.));
#30966=CARTESIAN_POINT('',(13.3800042915148,1.00338821889499E-5,4.45789143379912));
#30967=CARTESIAN_POINT('',(13.2699957084852,-6.83105689078257E-6,4.45784477598907));
#30968=CARTESIAN_POINT('',(12.5,-5.60735153159594E-17,4.457875));
#30969=CARTESIAN_POINT('Ctrl Pts',(13.2699957084852,-6.83105689078257E-6,
4.45784477598907));
#30970=CARTESIAN_POINT('Ctrl Pts',(13.265214377922,0.0458528260712244,4.45782008288951));
#30971=CARTESIAN_POINT('Ctrl Pts',(13.2604330473589,0.091719698604501,4.45096974854549));
#30972=CARTESIAN_POINT('Ctrl Pts',(13.2556517167957,0.135506404234727,4.43740478719402));
#30973=CARTESIAN_POINT('Ctrl Pts',(13.2477803447458,0.207591244700251,4.41507316710824));
#30974=CARTESIAN_POINT('Ctrl Pts',(13.2399089726958,0.274038390871736,4.37454348113122));
#30975=CARTESIAN_POINT('Ctrl Pts',(13.2320376006459,0.326885582178656,4.32067233995558));
#30976=CARTESIAN_POINT('Ctrl Pts',(13.2241662285959,0.379732773485576,4.26680119877995));
#30977=CARTESIAN_POINT('Ctrl Pts',(13.2162948565459,0.418980009927931,4.19958860240569));
#30978=CARTESIAN_POINT('Ctrl Pts',(13.208423484496,0.439924354792367,4.12708853413817));
#30979=CARTESIAN_POINT('Ctrl Pts',(13.200552112446,0.460868699656804,4.05458846587065));
#30980=CARTESIAN_POINT('Ctrl Pts',(13.1926807403961,0.463510152943321,3.97680092570987));
#30981=CARTESIAN_POINT('Ctrl Pts',(13.1848093683461,0.447532193317848,3.90304707640827));
#30982=CARTESIAN_POINT('Ctrl Pts',(13.1769379962962,0.431554233692375,3.82929322710668));
#30983=CARTESIAN_POINT('Ctrl Pts',(13.1690666242462,0.396956861154912,3.75957306866428));
#30984=CARTESIAN_POINT('Ctrl Pts',(13.1611952521963,0.347885826291745,3.70224106173923));
#30985=CARTESIAN_POINT('Ctrl Pts',(13.1533238801463,0.298814791428577,3.64490905481418));
#30986=CARTESIAN_POINT('Ctrl Pts',(13.1454525080963,0.235270094239705,3.59996519940648));
#30987=CARTESIAN_POINT('Ctrl Pts',(13.1375811360464,0.164866199243897,3.57279504942506));
#30988=CARTESIAN_POINT('Ctrl Pts',(13.1297097639964,0.0944623042480882,
3.54562489944363));
#30989=CARTESIAN_POINT('Ctrl Pts',(13.1218383919465,0.0171992114453437,
3.53622845488849));
#30990=CARTESIAN_POINT('Ctrl Pts',(13.1139670198965,-0.0576647601420857,
3.54573167743434));
#30991=CARTESIAN_POINT('Ctrl Pts',(13.1060956478466,-0.132528731729515,
3.55523489998019));
#30992=CARTESIAN_POINT('Ctrl Pts',(13.0982242757966,-0.204993582101629,
3.58363778962703));
#30993=CARTESIAN_POINT('Ctrl Pts',(13.0903529037467,-0.266375958336211,
3.62753687126191));
#30994=CARTESIAN_POINT('Ctrl Pts',(13.0824815316967,-0.327758334570793,
3.67143595289679));
#30995=CARTESIAN_POINT('Ctrl Pts',(13.0746101596467,-0.378058236667844,
3.73083122651971));
#30996=CARTESIAN_POINT('Ctrl Pts',(13.0667387875968,-0.411248303781717,
3.79860544673343));
#30997=CARTESIAN_POINT('Ctrl Pts',(13.0588674155468,-0.444438370895591,
3.86637966694714));
#30998=CARTESIAN_POINT('Ctrl Pts',(13.0509960434969,-0.460518603026287,
3.94253283375165));
#30999=CARTESIAN_POINT('Ctrl Pts',(13.0431246714469,-0.457562130387816,
4.0179396288708));
#31000=CARTESIAN_POINT('Ctrl Pts',(13.035253299397,-0.454605657749345,4.09334642398995));
#31001=CARTESIAN_POINT('Ctrl Pts',(13.027381927347,-0.432612480341706,4.16800684742375));
#31002=CARTESIAN_POINT('Ctrl Pts',(13.0195105552971,-0.394218007200806,
4.23297445406563));
#31003=CARTESIAN_POINT('Ctrl Pts',(13.0116391832471,-0.355823534059905,
4.29794206070751));
#31004=CARTESIAN_POINT('Ctrl Pts',(13.0037678111972,-0.301027765185743,
4.35321685055749));
#31005=CARTESIAN_POINT('Ctrl Pts',(12.9958964391472,-0.236396794305188,
4.39217532952931));
#31006=CARTESIAN_POINT('Ctrl Pts',(12.9880250670972,-0.171765823424632,
4.43113380850113));
#31007=CARTESIAN_POINT('Ctrl Pts',(12.9801536950473,-0.0972996505376846,
4.45377597659478));
#31008=CARTESIAN_POINT('Ctrl Pts',(12.9722823229973,-0.0219214440120968,
4.4573886572069));
#31009=CARTESIAN_POINT('Ctrl Pts',(12.9715201181599,-0.014622381881285,
4.45773848219561));
#31010=CARTESIAN_POINT('Ctrl Pts',(12.9707579133226,-0.00731476803234869,
4.45790987647069));
#31011=CARTESIAN_POINT('Ctrl Pts',(12.9699957084852,-6.90274666573233E-6,
4.45790451736119));
#31012=CARTESIAN_POINT('Ctrl Pts',(13.0800042915148,2.8196954984682E-6,
4.45783894202495));
#31013=CARTESIAN_POINT('Ctrl Pts',(13.084269570097,-0.0409086678841046,
4.4578299978409));
#31014=CARTESIAN_POINT('Ctrl Pts',(13.0885348486792,-0.0818224858219862,
4.45239605085009));
#31015=CARTESIAN_POINT('Ctrl Pts',(13.0928001272613,-0.121255029803553,
4.44156782927524));
#31016=CARTESIAN_POINT('Ctrl Pts',(13.1006714993113,-0.194025944662995,
4.42158485301405));
#31017=CARTESIAN_POINT('Ctrl Pts',(13.1085428713613,-0.261752088439453,
4.3832306090213));
#31018=CARTESIAN_POINT('Ctrl Pts',(13.1164142434112,-0.31631794022257,4.33110102808186));
#31019=CARTESIAN_POINT('Ctrl Pts',(13.1242856154612,-0.370883792005687,
4.27897144714243));
#31020=CARTESIAN_POINT('Ctrl Pts',(13.1321569875111,-0.412289351795463,
4.21306652925631));
#31021=CARTESIAN_POINT('Ctrl Pts',(13.1400283595611,-0.435573054271055,
4.14128356060242));
#31022=CARTESIAN_POINT('Ctrl Pts',(13.147899731611,-0.458856756746647,4.06950059194853));
#31023=CARTESIAN_POINT('Ctrl Pts',(13.155771103661,-0.464018601908056,3.99183957252686));
#31024=CARTESIAN_POINT('Ctrl Pts',(13.1636424757109,-0.45044005369213,3.91760650430194));
#31025=CARTESIAN_POINT('Ctrl Pts',(13.1715138477609,-0.436861505476204,
3.84337343607703));
#31026=CARTESIAN_POINT('Ctrl Pts',(13.1793852198109,-0.404542563882944,
3.77256831904885));
#31027=CARTESIAN_POINT('Ctrl Pts',(13.1872565918608,-0.357355958580309,
3.7136756228145));
#31028=CARTESIAN_POINT('Ctrl Pts',(13.1951279639108,-0.310169353277673,
3.65478292658016));
#31029=CARTESIAN_POINT('Ctrl Pts',(13.2029993359607,-0.248115084265664,
3.60780265113964));
#31030=CARTESIAN_POINT('Ctrl Pts',(13.2108707080107,-0.178629020319019,
3.57836437152041));
#31031=CARTESIAN_POINT('Ctrl Pts',(13.2187420800606,-0.109142956372374,
3.54892609190117));
#31032=CARTESIAN_POINT('Ctrl Pts',(13.2266134521106,-0.0322250974910928,
3.53702980810322));
#31033=CARTESIAN_POINT('Ctrl Pts',(13.2344848241605,0.0429076061587562,
3.54410103373967));
#31034=CARTESIAN_POINT('Ctrl Pts',(13.2423561962105,0.118040309808605,3.55117225937612));
#31035=CARTESIAN_POINT('Ctrl Pts',(13.2502275682605,0.191387858227023,3.57721099444696));
#31036=CARTESIAN_POINT('Ctrl Pts',(13.2580989403104,0.254161126126225,3.61909705689013));
#31037=CARTESIAN_POINT('Ctrl Pts',(13.2659703123604,0.316934394025428,3.66098311933329));
#31038=CARTESIAN_POINT('Ctrl Pts',(13.2738416844103,0.369133381405416,3.71871650914877));
#31039=CARTESIAN_POINT('Ctrl Pts',(13.2817130564603,0.404503162915977,3.78537912195109));
#31040=CARTESIAN_POINT('Ctrl Pts',(13.2895844285102,0.43987294442654,3.85204173475342));
#31041=CARTESIAN_POINT('Ctrl Pts',(13.2974558005602,0.458413520067676,3.92763357054259));
#31042=CARTESIAN_POINT('Ctrl Pts',(13.3053271726101,0.457903200829578,4.00309657448501));
#31043=CARTESIAN_POINT('Ctrl Pts',(13.3131985446601,0.457392881591479,4.07855957842742));
#31044=CARTESIAN_POINT('Ctrl Pts',(13.3210699167101,0.437831667474148,4.15389375052308));
#31045=CARTESIAN_POINT('Ctrl Pts',(13.32894128876,0.401563549045306,4.22007191138728));
#31046=CARTESIAN_POINT('Ctrl Pts',(13.33681266081,0.365295430616463,4.28625007225149));
#31047=CARTESIAN_POINT('Ctrl Pts',(13.3446840328599,0.31232040787611,4.34327222188425));
#31048=CARTESIAN_POINT('Ctrl Pts',(13.3525554049099,0.248986397312635,4.38430548273058));
#31049=CARTESIAN_POINT('Ctrl Pts',(13.3604267769598,0.185652386749161,4.42533874357692));
#31050=CARTESIAN_POINT('Ctrl Pts',(13.3682981490098,0.111959388362564,4.45038311563682));
#31051=CARTESIAN_POINT('Ctrl Pts',(13.3761695210597,0.0367379221854645,
4.45643756985705));
#31052=CARTESIAN_POINT('Ctrl Pts',(13.3774477778781,0.024522472144774,4.45742077168506));
#31053=CARTESIAN_POINT('Ctrl Pts',(13.3787260346965,0.0122667140672706,
4.45790318029249));
#31054=CARTESIAN_POINT('Ctrl Pts',(13.3800042915148,1.00338821889499E-5,
4.45789143379912));
#31055=CARTESIAN_POINT('Origin',(12.5,0.,4.));
#31056=CARTESIAN_POINT('',(13.6800042915148,-8.85210990424201E-6,4.45789764648838));
#31057=CARTESIAN_POINT('',(13.5699957084852,1.03170790782398E-5,4.4578580083501));
#31058=CARTESIAN_POINT('',(12.5,-5.60735153159594E-17,4.457875));
#31059=CARTESIAN_POINT('Ctrl Pts',(13.5699957084852,1.03170790782398E-5,
4.4578580083501));
#31060=CARTESIAN_POINT('Ctrl Pts',(13.5675422145714,0.0235408097699949,
4.45787795556699));
#31061=CARTESIAN_POINT('Ctrl Pts',(13.5650887206577,0.0470683081483061,
4.45609516914004));
#31062=CARTESIAN_POINT('Ctrl Pts',(13.562635226744,0.0703115975725277,4.45248338388903));
#31063=CARTESIAN_POINT('Ctrl Pts',(13.554763854694,0.144881409096958,4.44089594716616));
#31064=CARTESIAN_POINT('Ctrl Pts',(13.5468924826441,0.21652593236894,4.41048310506186));
#31065=CARTESIAN_POINT('Ctrl Pts',(13.5390211105941,0.276660113016528,4.36488918223832));
#31066=CARTESIAN_POINT('Ctrl Pts',(13.5311497385442,0.336794293664116,4.31929525941478));
#31067=CARTESIAN_POINT('Ctrl Pts',(13.5232783664942,0.385418131687311,4.25852025587201));
#31068=CARTESIAN_POINT('Ctrl Pts',(13.5154069944443,0.416705106451492,4.18984674794718));
#31069=CARTESIAN_POINT('Ctrl Pts',(13.5075356223943,0.447992081215673,4.12117324002235));
#31070=CARTESIAN_POINT('Ctrl Pts',(13.4996642503443,0.461942192720839,4.04460122771548));
#31071=CARTESIAN_POINT('Ctrl Pts',(13.4917928782944,0.456883820300162,3.96930621892307));
#31072=CARTESIAN_POINT('Ctrl Pts',(13.4839215062444,0.451825447879485,3.89401121013066));
#31073=CARTESIAN_POINT('Ctrl Pts',(13.4760501341945,0.427758591532965,3.81999320485271));
#31074=CARTESIAN_POINT('Ctrl Pts',(13.4681787621445,0.387567146091087,3.75612166820384));
#31075=CARTESIAN_POINT('Ctrl Pts',(13.4603073900946,0.347375700649209,3.69225013155497));
#31076=CARTESIAN_POINT('Ctrl Pts',(13.4524360180446,0.291059666111973,3.63852506353517));
#31077=CARTESIAN_POINT('Ctrl Pts',(13.4445646459947,0.225367307335285,3.60138425741911));
#31078=CARTESIAN_POINT('Ctrl Pts',(13.4366932739447,0.159674948558598,3.56424345130305));
#31079=CARTESIAN_POINT('Ctrl Pts',(13.4288219018947,0.0846062655424597,
3.54368690709073));
#31080=CARTESIAN_POINT('Ctrl Pts',(13.4209505298448,0.00915662451852634,
3.54217788424291));
#31081=CARTESIAN_POINT('Ctrl Pts',(13.4130791577948,-0.0662930165054059,
3.54066886139509));
#31082=CARTESIAN_POINT('Ctrl Pts',(13.4052077857449,-0.142123615537132,
3.55820735991178));
#31083=CARTESIAN_POINT('Ctrl Pts',(13.3973364136949,-0.209248507106454,
3.5926917681625));
#31084=CARTESIAN_POINT('Ctrl Pts',(13.389465041645,-0.276373398675776,3.62717617641322));
#31085=CARTESIAN_POINT('Ctrl Pts',(13.381593669595,-0.334792582782693,3.67860649439798));
#31086=CARTESIAN_POINT('Ctrl Pts',(13.3737222975451,-0.377505777353741,
3.74081990525232));
#31087=CARTESIAN_POINT('Ctrl Pts',(13.3658509254951,-0.420218971924789,
3.80303331610666));
#31088=CARTESIAN_POINT('Ctrl Pts',(13.3579795534451,-0.44722617695997,3.87602981983059));
#31089=CARTESIAN_POINT('Ctrl Pts',(13.3501081813952,-0.455291160112798,
3.95106235628872));
#31090=CARTESIAN_POINT('Ctrl Pts',(13.3422368093452,-0.463356143265626,
4.02609489274685));
#31091=CARTESIAN_POINT('Ctrl Pts',(13.3343654372953,-0.452478904536101,
4.10316346193917));
#31092=CARTESIAN_POINT('Ctrl Pts',(13.3264940652453,-0.423962846915058,
4.17303305431203));
#31093=CARTESIAN_POINT('Ctrl Pts',(13.3186226931954,-0.395446789294015,
4.24290264668488));
#31094=CARTESIAN_POINT('Ctrl Pts',(13.3107513211454,-0.349291912781453,
4.30557326223827));
#31095=CARTESIAN_POINT('Ctrl Pts',(13.3028799490955,-0.291028886105345,
4.35353517632783));
#31096=CARTESIAN_POINT('Ctrl Pts',(13.2950085770455,-0.232765859429236,
4.4014970904174));
#31097=CARTESIAN_POINT('Ctrl Pts',(13.2871372049956,-0.162394682589579,
4.43475030304313));
#31098=CARTESIAN_POINT('Ctrl Pts',(13.2792658329456,-0.0883478267899694,
4.44931013225873));
#31099=CARTESIAN_POINT('Ctrl Pts',(13.2761757914588,-0.059279469337623,
4.4550258417985));
#31100=CARTESIAN_POINT('Ctrl Pts',(13.273085749972,-0.0296446570187532,
4.45786073445524));
#31101=CARTESIAN_POINT('Ctrl Pts',(13.2699957084852,-6.83105689078257E-6,
4.45784477598907));
#31102=CARTESIAN_POINT('Ctrl Pts',(13.3800042915148,1.00338821889499E-5,
4.45789143379912));
#31103=CARTESIAN_POINT('Ctrl Pts',(13.3865974067464,-0.0632086430349686,
4.45783084661254));
#31104=CARTESIAN_POINT('Ctrl Pts',(13.393190521978,-0.12645185159805,4.44462381290384));
#31105=CARTESIAN_POINT('Ctrl Pts',(13.3997836372096,-0.184315051738561,
4.41918121595096));
#31106=CARTESIAN_POINT('Ctrl Pts',(13.4076550092596,-0.253396625517876,
4.3888058714441));
#31107=CARTESIAN_POINT('Ctrl Pts',(13.4155263813095,-0.314809839108902,
4.34099064604983));
#31108=CARTESIAN_POINT('Ctrl Pts',(13.4233977533595,-0.361195640434018,
4.28146516557999));
#31109=CARTESIAN_POINT('Ctrl Pts',(13.4312691254094,-0.407581441759134,
4.22193968511016));
#31110=CARTESIAN_POINT('Ctrl Pts',(13.4391404974594,-0.438939830818339,
4.15070394956476));
#31111=CARTESIAN_POINT('Ctrl Pts',(13.4470118695093,-0.451513179494438,
4.07629402890356));
#31112=CARTESIAN_POINT('Ctrl Pts',(13.4548832415593,-0.464086528170537,
4.00188410824235));
#31113=CARTESIAN_POINT('Ctrl Pts',(13.4627546136093,-0.457874836463529,
3.92430000246534));
#31114=CARTESIAN_POINT('Ctrl Pts',(13.4706259856592,-0.433622441953051,
3.85283849709185));
#31115=CARTESIAN_POINT('Ctrl Pts',(13.4784973577092,-0.409370047442573,
3.78137699171835));
#31116=CARTESIAN_POINT('Ctrl Pts',(13.4863687297591,-0.367076950128625,
3.71603808674838));
#31117=CARTESIAN_POINT('Ctrl Pts',(13.4942401018091,-0.311811067605128,
3.66465124389307));
#31118=CARTESIAN_POINT('Ctrl Pts',(13.502111473859,-0.25654518508163,3.61326440103776));
#31119=CARTESIAN_POINT('Ctrl Pts',(13.509982845909,-0.188306517348584,3.5758296202971));
#31120=CARTESIAN_POINT('Ctrl Pts',(13.5178542179589,-0.115272000283325,
3.55683265457144));
#31121=CARTESIAN_POINT('Ctrl Pts',(13.5257255900089,-0.0422374832180674,
3.53783568884578));
#31122=CARTESIAN_POINT('Ctrl Pts',(13.5335969620589,0.035592883179403,3.53727653813511));
#31123=CARTESIAN_POINT('Ctrl Pts',(13.5414683341088,0.108892804353757,3.55522220461956));
#31124=CARTESIAN_POINT('Ctrl Pts',(13.5493397061588,0.182192725528112,3.573167871104));
#31125=CARTESIAN_POINT('Ctrl Pts',(13.5572110782087,0.250962201479351,3.60961835478357));
#31126=CARTESIAN_POINT('Ctrl Pts',(13.5650824502587,0.306960690387823,3.66020584957927));
#31127=CARTESIAN_POINT('Ctrl Pts',(13.5729538223086,0.362959179296295,3.71079334437498));
#31128=CARTESIAN_POINT('Ctrl Pts',(13.5808251943586,0.406186681162,3.77551785028682));
#31129=CARTESIAN_POINT('Ctrl Pts',(13.5886965664085,0.431463310113251,3.84662352810933));
#31130=CARTESIAN_POINT('Ctrl Pts',(13.5965679384585,0.456739939064502,3.91772920593184));
#31131=CARTESIAN_POINT('Ctrl Pts',(13.6044393105085,0.464065695101298,3.99521605566501));
#31132=CARTESIAN_POINT('Ctrl Pts',(13.6123106825584,0.452562744007997,4.06979894583348));
#31133=CARTESIAN_POINT('Ctrl Pts',(13.6201820546084,0.441059792914696,4.14438183600196));
#31134=CARTESIAN_POINT('Ctrl Pts',(13.6280534266583,0.410728134691299,4.21606076660573));
#31135=CARTESIAN_POINT('Ctrl Pts',(13.6359247987083,0.365202365858889,4.27624656029457));
#31136=CARTESIAN_POINT('Ctrl Pts',(13.6437961707582,0.319676597026479,4.33643235398341));
#31137=CARTESIAN_POINT('Ctrl Pts',(13.6516675428082,0.258956717585058,4.38512501075732));
#31138=CARTESIAN_POINT('Ctrl Pts',(13.6595389148581,0.190318698434502,4.41648976353532));
#31139=CARTESIAN_POINT('Ctrl Pts',(13.666360707077,0.130832969391341,4.44367229602021));
#31140=CARTESIAN_POINT('Ctrl Pts',(13.6731824992959,0.065399948454096,4.45783988979956));
#31141=CARTESIAN_POINT('Ctrl Pts',(13.6800042915148,-8.85210990424201E-6,
4.45789764648838));
#31142=CARTESIAN_POINT('Origin',(12.5,0.,4.));
#31143=CARTESIAN_POINT('',(13.9800042915148,-4.68615130337092E-6,4.45784092071359));
#31144=CARTESIAN_POINT('',(13.8699957084852,1.23414887176878E-6,4.4579133809027));
#31145=CARTESIAN_POINT('',(12.5,-5.60735153159594E-17,4.457875));
#31146=CARTESIAN_POINT('Ctrl Pts',(13.8699957084852,1.23414887176878E-6,
4.4579133809027));
#31147=CARTESIAN_POINT('Ctrl Pts',(13.8698700512209,0.00120594270822336,
4.45791357044259));
#31148=CARTESIAN_POINT('Ctrl Pts',(13.8697443939566,0.00241064979645091,
4.45790891401425));
#31149=CARTESIAN_POINT('Ctrl Pts',(13.8696187366923,0.00361531855258033,
4.45789940262096));
#31150=CARTESIAN_POINT('Ctrl Pts',(13.8617473646423,0.0790776965455978,
4.45730359373015));
#31151=CARTESIAN_POINT('Ctrl Pts',(13.8538759925924,0.154389660535011,4.43765704798318));
#31152=CARTESIAN_POINT('Ctrl Pts',(13.8460046205424,0.22052669229976,4.40131398110731));
#31153=CARTESIAN_POINT('Ctrl Pts',(13.8381332484924,0.286663724064511,4.36497091423144));
#31154=CARTESIAN_POINT('Ctrl Pts',(13.8302618764425,0.343625823604597,4.31193132622667));
#31155=CARTESIAN_POINT('Ctrl Pts',(13.8223905043925,0.384587309076409,4.24855087033892));
#31156=CARTESIAN_POINT('Ctrl Pts',(13.8145191323426,0.42554879454822,4.18517041445118));
#31157=CARTESIAN_POINT('Ctrl Pts',(13.8066477602926,0.450509665951756,4.11144909068046));
#31158=CARTESIAN_POINT('Ctrl Pts',(13.7987763882427,0.456478899990553,4.03622081324714));
#31159=CARTESIAN_POINT('Ctrl Pts',(13.7909050161927,0.46244813402935,3.96099253581381));
#31160=CARTESIAN_POINT('Ctrl Pts',(13.7830336441427,0.449425730703409,3.88425730471787));
#31161=CARTESIAN_POINT('Ctrl Pts',(13.7751622720928,0.418972144817937,3.81521018611534));
#31162=CARTESIAN_POINT('Ctrl Pts',(13.7672909000428,0.388518558932466,3.74616306751281));
#31163=CARTESIAN_POINT('Ctrl Pts',(13.7594195279929,0.340633790487464,3.68480406140369));
#31164=CARTESIAN_POINT('Ctrl Pts',(13.7515481559429,0.281055798532888,3.6384857242654));
#31165=CARTESIAN_POINT('Ctrl Pts',(13.743676783893,0.221477806578313,3.59216738712712));
#31166=CARTESIAN_POINT('Ctrl Pts',(13.735805411843,0.150206591114165,3.56088971895966));
#31167=CARTESIAN_POINT('Ctrl Pts',(13.7279340397931,0.0757824736049535,
3.54840067521841));
#31168=CARTESIAN_POINT('Ctrl Pts',(13.7200626677431,0.00135835609574232,
3.53591163147717));
#31169=CARTESIAN_POINT('Ctrl Pts',(13.7121912956931,-0.0762186634585312,
3.54221121216214));
#31170=CARTESIAN_POINT('Ctrl Pts',(13.7043199236432,-0.14765264866984,3.56654454809098));
#31171=CARTESIAN_POINT('Ctrl Pts',(13.6964485515932,-0.219086633881149,
3.59087788401983));
#31172=CARTESIAN_POINT('Ctrl Pts',(13.6885771795433,-0.284377584749494,
3.63324497519255));
#31173=CARTESIAN_POINT('Ctrl Pts',(13.6807058074933,-0.335701785830877,
3.68856903744356));
#31174=CARTESIAN_POINT('Ctrl Pts',(13.6728344354434,-0.38702598691226,3.74389309969457));
#31175=CARTESIAN_POINT('Ctrl Pts',(13.6649630633934,-0.424383438206683,
3.81217413302386));
#31176=CARTESIAN_POINT('Ctrl Pts',(13.6570916913435,-0.443297653083863,
3.88523012494906));
#31177=CARTESIAN_POINT('Ctrl Pts',(13.6492203192935,-0.462211867961044,
3.95828611687427));
#31178=CARTESIAN_POINT('Ctrl Pts',(13.6413489472436,-0.462682846420982,
4.03611706739538));
#31179=CARTESIAN_POINT('Ctrl Pts',(13.6334775751936,-0.444654151830396,
4.10939661196244));
#31180=CARTESIAN_POINT('Ctrl Pts',(13.6256062031436,-0.42662545723981,4.18267615652949));
#31181=CARTESIAN_POINT('Ctrl Pts',(13.6177348310937,-0.3900970895987,4.25140429514248));
#31182=CARTESIAN_POINT('Ctrl Pts',(13.6098634590437,-0.339446187702822,
4.3073454393722));
#31183=CARTESIAN_POINT('Ctrl Pts',(13.6019920869938,-0.288795285806945,
4.36328658360191));
#31184=CARTESIAN_POINT('Ctrl Pts',(13.5941207149438,-0.224021849656302,
4.40644073344835));
#31185=CARTESIAN_POINT('Ctrl Pts',(13.5862493428939,-0.152887581692542,
4.43163679270085));
#31186=CARTESIAN_POINT('Ctrl Pts',(13.5808314647576,-0.103925749791867,
4.44897928111035));
#31187=CARTESIAN_POINT('Ctrl Pts',(13.5754135866214,-0.0519504158054226,
4.45781396031326));
#31188=CARTESIAN_POINT('Ctrl Pts',(13.5699957084852,1.03170790782398E-5,
4.4578580083501));
#31189=CARTESIAN_POINT('Ctrl Pts',(13.6800042915148,-8.85210990424201E-6,
4.45789764648838));
#31190=CARTESIAN_POINT('Ctrl Pts',(13.6810538713459,-0.010072447664127,
4.45790653275371));
#31191=CARTESIAN_POINT('Ctrl Pts',(13.6821034511769,-0.0201354698749596,
4.45758141170421));
#31192=CARTESIAN_POINT('Ctrl Pts',(13.683153031008,-0.0301761699425476,
4.45691829561871));
#31193=CARTESIAN_POINT('Ctrl Pts',(13.691024403058,-0.105476860309351,4.45194522614199));
#31194=CARTESIAN_POINT('Ctrl Pts',(13.6988957751079,-0.179522082183268,
4.42796223840642));
#31195=CARTESIAN_POINT('Ctrl Pts',(13.7067671471579,-0.24343910912634,4.38784317739428));
#31196=CARTESIAN_POINT('Ctrl Pts',(13.7146385192078,-0.307356136069411,
4.34772411638213));
#31197=CARTESIAN_POINT('Ctrl Pts',(13.7225098912578,-0.361144968081636,
4.2914689820934));
#31198=CARTESIAN_POINT('Ctrl Pts',(13.7303812633077,-0.398360171146024,
4.22581874179975));
#31199=CARTESIAN_POINT('Ctrl Pts',(13.7382526353577,-0.435575374210412,
4.1601685015061));
#31200=CARTESIAN_POINT('Ctrl Pts',(13.7461240074077,-0.456216948326962,
4.08512315520753));
#31201=CARTESIAN_POINT('Ctrl Pts',(13.7539953794576,-0.457811445030669,
4.00967527273228));
#31202=CARTESIAN_POINT('Ctrl Pts',(13.7618667515076,-0.459405941734377,
3.93422739025703));
#31203=CARTESIAN_POINT('Ctrl Pts',(13.7697381235575,-0.441953361025241,
3.85837697160509));
#31204=CARTESIAN_POINT('Ctrl Pts',(13.7776094956075,-0.407545019133394,
3.79121305720166));
#31205=CARTESIAN_POINT('Ctrl Pts',(13.7854808676574,-0.373136677241547,
3.72404914279823));
#31206=CARTESIAN_POINT('Ctrl Pts',(13.7933522397074,-0.321772574166988,
3.6655717326433));
#31207=CARTESIAN_POINT('Ctrl Pts',(13.8012236117573,-0.259607592342073,
3.6227880859492));
#31208=CARTESIAN_POINT('Ctrl Pts',(13.8090949838073,-0.19744261051716,3.5800044392551));
#31209=CARTESIAN_POINT('Ctrl Pts',(13.8169663558573,-0.124476749941891,
3.55291455602183));
#31210=CARTESIAN_POINT('Ctrl Pts',(13.8248377279072,-0.0494533988297167,
3.54476457579874));
#31211=CARTESIAN_POINT('Ctrl Pts',(13.8327090999572,0.0255699522824598,
3.53661459557564));
#31212=CARTESIAN_POINT('Ctrl Pts',(13.8405804720071,0.102650793931542,3.54740451836272));
#31213=CARTESIAN_POINT('Ctrl Pts',(13.8484518440571,0.172552645974024,3.57584140410587));
#31214=CARTESIAN_POINT('Ctrl Pts',(13.856323216107,0.242454498016503,3.60427828984902));
#31215=CARTESIAN_POINT('Ctrl Pts',(13.864194588157,0.305177360452382,3.65036213854823));
#31216=CARTESIAN_POINT('Ctrl Pts',(13.8720659602069,0.353205247972751,3.70857079263049));
#31217=CARTESIAN_POINT('Ctrl Pts',(13.8799373322569,0.40123313549312,3.76677944671275));
#31218=CARTESIAN_POINT('Ctrl Pts',(13.8878087043068,0.434566048097978,3.83711290617806));
#31219=CARTESIAN_POINT('Ctrl Pts',(13.8956800763568,0.44920975351361,3.9111432194385));
#31220=CARTESIAN_POINT('Ctrl Pts',(13.9035514484068,0.463853458929242,3.98517353269893));
#31221=CARTESIAN_POINT('Ctrl Pts',(13.9114228204567,0.459807957155645,4.06290069975448));
#31222=CARTESIAN_POINT('Ctrl Pts',(13.9192941925067,0.437558014523894,4.13501079227018));
#31223=CARTESIAN_POINT('Ctrl Pts',(13.9271655645566,0.415308071892144,4.20712088478587));
#31224=CARTESIAN_POINT('Ctrl Pts',(13.9350369366066,0.374853688402242,4.27361390276169));
#31225=CARTESIAN_POINT('Ctrl Pts',(13.9429083086565,0.321042451364188,4.32652208887851));
#31226=CARTESIAN_POINT('Ctrl Pts',(13.9507796807065,0.267231214326134,4.37943027499533));
#31227=CARTESIAN_POINT('Ctrl Pts',(13.9586510527564,0.200063123739928,4.41875362925314));
#31228=CARTESIAN_POINT('Ctrl Pts',(13.9665224248064,0.127586829849962,4.43978009385641));
#31229=CARTESIAN_POINT('Ctrl Pts',(13.9710163803759,0.086208370984788,4.45178460807712));
#31230=CARTESIAN_POINT('Ctrl Pts',(13.9755103359454,0.0430996806131821,
4.45782517307841));
#31231=CARTESIAN_POINT('Ctrl Pts',(13.9800042915148,-4.68615130337092E-6,
4.45784092071359));
#31232=CARTESIAN_POINT('Origin',(12.5,0.,4.));
#31233=CARTESIAN_POINT('',(14.2800042915148,1.11332528513013E-5,4.45786561359635));
#31234=CARTESIAN_POINT('',(14.1699957084852,-1.10604184835328E-5,4.4578646218584));
#31235=CARTESIAN_POINT('',(12.5,-5.60735153159594E-17,4.457875));
#31236=CARTESIAN_POINT('Ctrl Pts',(14.1699957084852,-1.10604184835328E-5,
4.4578646218584));
#31237=CARTESIAN_POINT('Ctrl Pts',(14.1643265158203,0.0543576752587709,
4.45781404039958));
#31238=CARTESIAN_POINT('Ctrl Pts',(14.1586573231555,0.108743966382031,4.44812254260427));
#31239=CARTESIAN_POINT('Ctrl Pts',(14.1529881304907,0.159684023833442,4.42916890146099));
#31240=CARTESIAN_POINT('Ctrl Pts',(14.1451167584407,0.230411580321883,4.40285278028461));
#31241=CARTESIAN_POINT('Ctrl Pts',(14.1372453863907,0.294495541512382,4.358681244225));
#31242=CARTESIAN_POINT('Ctrl Pts',(14.1293740143408,0.344256823700223,4.30194730133701));
#31243=CARTESIAN_POINT('Ctrl Pts',(14.1215026422908,0.394018105888063,4.24521335844902));
#31244=CARTESIAN_POINT('Ctrl Pts',(14.1136312702409,0.429456709073245,4.17591700873265));
#31245=CARTESIAN_POINT('Ctrl Pts',(14.1057598981909,0.446326079279053,4.10236192849032));
#31246=CARTESIAN_POINT('Ctrl Pts',(14.097888526141,0.46319544948486,4.02880684824799));
#31247=CARTESIAN_POINT('Ctrl Pts',(14.090017154091,0.461495586711293,3.95099303747972));
#31248=CARTESIAN_POINT('Ctrl Pts',(14.0821457820411,0.441430182931853,3.87824480690492));
#31249=CARTESIAN_POINT('Ctrl Pts',(14.0742744099911,0.421364779152413,3.80549657633012));
#31250=CARTESIAN_POINT('Ctrl Pts',(14.0664030379411,0.3829338343671,3.73781392594881));
#31251=CARTESIAN_POINT('Ctrl Pts',(14.0585316658912,0.330742470300218,3.68330716492384));
#31252=CARTESIAN_POINT('Ctrl Pts',(14.0506602938412,0.278551106233337,3.62880040389886));
#31253=CARTESIAN_POINT('Ctrl Pts',(14.0427889217913,0.212599322884887,3.58746953223022));
#31254=CARTESIAN_POINT('Ctrl Pts',(14.0349175497413,0.140790022250932,3.5642671654747));
#31255=CARTESIAN_POINT('Ctrl Pts',(14.0270461776914,0.0689807216169763,
3.54106479871918));
#31256=CARTESIAN_POINT('Ctrl Pts',(14.0191748056414,-0.00868609630248519,
3.53599093687678));
#31257=CARTESIAN_POINT('Ctrl Pts',(14.0113034335915,-0.0829037347177578,
3.5496535731032));
#31258=CARTESIAN_POINT('Ctrl Pts',(14.0034320615415,-0.15712137313303,3.56331620932962));
#31259=CARTESIAN_POINT('Ctrl Pts',(13.9955606894916,-0.227889832044114,
3.59571534362485));
#31260=CARTESIAN_POINT('Ctrl Pts',(13.9876893174416,-0.286729034540398,
3.64296863695132));
#31261=CARTESIAN_POINT('Ctrl Pts',(13.9798179453916,-0.345568237036683,
3.69022193027778));
#31262=CARTESIAN_POINT('Ctrl Pts',(13.9719465733417,-0.392478183118168,
3.75232938263547));
#31263=CARTESIAN_POINT('Ctrl Pts',(13.9640752012917,-0.421837725217638,
3.82184875237013));
#31264=CARTESIAN_POINT('Ctrl Pts',(13.9562038292418,-0.451197267317109,
3.8913681221048));
#31265=CARTESIAN_POINT('Ctrl Pts',(13.9483324571918,-0.463006405434566,
3.96829940921644));
#31266=CARTESIAN_POINT('Ctrl Pts',(13.9404610851419,-0.455850068491383,
4.04342405445454));
#31267=CARTESIAN_POINT('Ctrl Pts',(13.9325897130919,-0.448693731548199,
4.11854869969265));
#31268=CARTESIAN_POINT('Ctrl Pts',(13.924718341042,-0.422571919544373,4.19186670305722));
#31269=CARTESIAN_POINT('Ctrl Pts',(13.916846968992,-0.38061476952465,4.25459247959939));
#31270=CARTESIAN_POINT('Ctrl Pts',(13.908975596942,-0.338657619504927,4.31731825614156));
#31271=CARTESIAN_POINT('Ctrl Pts',(13.9011042248921,-0.280865131469307,
4.36945180586132));
#31272=CARTESIAN_POINT('Ctrl Pts',(13.8932328528421,-0.214162491453186,
4.40474604470388));
#31273=CARTESIAN_POINT('Ctrl Pts',(13.8854871380565,-0.148524681204106,
4.43947685223224));
#31274=CARTESIAN_POINT('Ctrl Pts',(13.8777414232708,-0.0742589286223064,
4.45790169736071));
#31275=CARTESIAN_POINT('Ctrl Pts',(13.8699957084852,1.23414887176878E-6,
4.4579133809027));
#31276=CARTESIAN_POINT('Ctrl Pts',(13.9800042915148,-4.68615130337092E-6,
4.45784092071359));
#31277=CARTESIAN_POINT('Ctrl Pts',(13.9833817079953,-0.0323996211791616,
4.45785275579335));
#31278=CARTESIAN_POINT('Ctrl Pts',(13.9867591244758,-0.064792114138131,
4.45446164082457));
#31279=CARTESIAN_POINT('Ctrl Pts',(13.9901365409563,-0.0964458636128916,
4.44764173788363));
#31280=CARTESIAN_POINT('Ctrl Pts',(13.9980079130062,-0.170217765992045,
4.43174734235885));
#31281=CARTESIAN_POINT('Ctrl Pts',(14.0058792850562,-0.239977073556624,
4.39722897636055));
#31282=CARTESIAN_POINT('Ctrl Pts',(14.0137506571061,-0.297364634468633,
4.34822292324149));
#31283=CARTESIAN_POINT('Ctrl Pts',(14.0216220291561,-0.354752195380644,
4.29921687012243));
#31284=CARTESIAN_POINT('Ctrl Pts',(14.0294934012061,-0.399768009640084,
4.23572312988262));
#31285=CARTESIAN_POINT('Ctrl Pts',(14.037364773256,-0.427017900618165,4.16535006094698));
#31286=CARTESIAN_POINT('Ctrl Pts',(14.045236145306,-0.454267791596245,4.09497699201134));
#31287=CARTESIAN_POINT('Ctrl Pts',(14.0531075173559,-0.463751759292965,
4.01772459437987));
#31288=CARTESIAN_POINT('Ctrl Pts',(14.0609788894059,-0.45433335426851,3.94284990548881));
#31289=CARTESIAN_POINT('Ctrl Pts',(14.0688502614558,-0.444914949244056,
3.86797521659775));
#31290=CARTESIAN_POINT('Ctrl Pts',(14.0767216335058,-0.416594171498428,
3.7954782364471));
#31291=CARTESIAN_POINT('Ctrl Pts',(14.0845930055557,-0.372764656800254,
3.7340461680214));
#31292=CARTESIAN_POINT('Ctrl Pts',(14.0924643776057,-0.328935142102078,
3.67261409959569));
#31293=CARTESIAN_POINT('Ctrl Pts',(14.1003357496557,-0.269596890451354,
3.62224694289495));
#31294=CARTESIAN_POINT('Ctrl Pts',(14.1082071217056,-0.201860314388951,
3.58898011778223));
#31295=CARTESIAN_POINT('Ctrl Pts',(14.1160784937556,-0.134123738326549,
3.55571329266952));
#31296=CARTESIAN_POINT('Ctrl Pts',(14.1239498658055,-0.0579888378524715,
3.53954679914483));
#31297=CARTESIAN_POINT('Ctrl Pts',(14.1318212378555,0.0174212575835846,
3.54241784356498));
#31298=CARTESIAN_POINT('Ctrl Pts',(14.1396926099054,0.0928313530196406,
3.54528888798513));
#31299=CARTESIAN_POINT('Ctrl Pts',(14.1475639819554,0.167516643417675,3.56719747035013));
#31300=CARTESIAN_POINT('Ctrl Pts',(14.1554353540053,0.232527703900953,3.60551831852155));
#31301=CARTESIAN_POINT('Ctrl Pts',(14.1633067260553,0.297538764384231,3.64383916669297));
#31302=CARTESIAN_POINT('Ctrl Pts',(14.1711780981053,0.352875594952755,3.69857228067082));
#31303=CARTESIAN_POINT('Ctrl Pts',(14.1790494701552,0.391907267274456,3.76315907456484));
#31304=CARTESIAN_POINT('Ctrl Pts',(14.1869208422052,0.430938939596158,3.82774586845886));
#31305=CARTESIAN_POINT('Ctrl Pts',(14.1947922142551,0.453665453671035,3.90218634226906));
#31306=CARTESIAN_POINT('Ctrl Pts',(14.2026635863051,0.45736352584659,3.97756040711846));
#31307=CARTESIAN_POINT('Ctrl Pts',(14.210534958355,0.461061598022145,4.05293447196787));
#31308=CARTESIAN_POINT('Ctrl Pts',(14.218406330405,0.445731228298378,4.12924212785648));
#31309=CARTESIAN_POINT('Ctrl Pts',(14.2262777024549,0.413209431587385,4.19733954431574));
#31310=CARTESIAN_POINT('Ctrl Pts',(14.2341490745049,0.380687634876391,4.265436960775));
#31311=CARTESIAN_POINT('Ctrl Pts',(14.2420204465549,0.330974411178171,4.32532413780492));
#31312=CARTESIAN_POINT('Ctrl Pts',(14.2498918186048,0.270026820557645,4.36982488597043));
#31313=CARTESIAN_POINT('Ctrl Pts',(14.2577631906548,0.209079229937118,4.41432563413594));
#31314=CARTESIAN_POINT('Ctrl Pts',(14.2656345627047,0.136897272394287,4.44343995343705));
#31315=CARTESIAN_POINT('Ctrl Pts',(14.2735059347547,0.0621304022332317,
4.45367911922619));
#31316=CARTESIAN_POINT('Ctrl Pts',(14.2756720536747,0.0415553447945806,
4.4564968301158));
#31317=CARTESIAN_POINT('Ctrl Pts',(14.2778381725948,0.020784533837212,4.45788513960506));
#31318=CARTESIAN_POINT('Ctrl Pts',(14.2800042915148,1.11332528513013E-5,
4.45786561359635));
#31319=CARTESIAN_POINT('Origin',(12.5,0.,4.));
#31320=CARTESIAN_POINT('',(14.5800042915148,-1.58578451148518E-6,4.45791318879952));
#31321=CARTESIAN_POINT('',(14.4699957084852,4.96934848862042E-6,4.4578413260902));
#31322=CARTESIAN_POINT('',(12.5,-5.60735153159594E-17,4.457875));
#31323=CARTESIAN_POINT('Ctrl Pts',(14.4699957084852,4.96934848862042E-6,
4.4578413260902));
#31324=CARTESIAN_POINT('Ctrl Pts',(14.4666543524698,0.0320539454002899,
4.45785375637851));
#31325=CARTESIAN_POINT('Ctrl Pts',(14.4633129964543,0.0641003838712636,
4.45453523052653));
#31326=CARTESIAN_POINT('Ctrl Pts',(14.4599716404389,0.0954313752779353,
4.44785911407655));
#31327=CARTESIAN_POINT('Ctrl Pts',(14.452100268389,0.169239101517837,4.43213190746217));
#31328=CARTESIAN_POINT('Ctrl Pts',(14.444228896339,0.2390764403586,4.39777168651743));
#31329=CARTESIAN_POINT('Ctrl Pts',(14.4363575242891,0.296574889592956,4.34889578431359));
#31330=CARTESIAN_POINT('Ctrl Pts',(14.4284861522391,0.354073338827311,4.30001988210975));
#31331=CARTESIAN_POINT('Ctrl Pts',(14.4206147801891,0.39923289845526,4.2366282986468));
#31332=CARTESIAN_POINT('Ctrl Pts',(14.4127434081392,0.4266421670589,4.16631715105832));
#31333=CARTESIAN_POINT('Ctrl Pts',(14.4048720360892,0.454051435662541,4.09600600346984));
#31334=CARTESIAN_POINT('Ctrl Pts',(14.3970006640393,0.463710413241873,4.01877529175582));
#31335=CARTESIAN_POINT('Ctrl Pts',(14.3891292919893,0.454461679188747,3.94387945476197));
#31336=CARTESIAN_POINT('Ctrl Pts',(14.3812579199394,0.445212945135621,3.86898361776811));
#31337=CARTESIAN_POINT('Ctrl Pts',(14.3733865478894,0.417056499450037,3.79642265549441));
#31338=CARTESIAN_POINT('Ctrl Pts',(14.3655151758395,0.373366286239542,3.73489143780602));
#31339=CARTESIAN_POINT('Ctrl Pts',(14.3576438037895,0.329676073029047,3.67336022011762));
#31340=CARTESIAN_POINT('Ctrl Pts',(14.3497724317395,0.270452092293641,3.62285874701452));
#31341=CARTESIAN_POINT('Ctrl Pts',(14.3419010596896,0.202791063664024,3.58943853329022));
#31342=CARTESIAN_POINT('Ctrl Pts',(14.3340296876396,0.135130035034407,3.55601831956592));
#31343=CARTESIAN_POINT('Ctrl Pts',(14.3261583155897,0.0590319585105798,
3.53967936522043));
#31344=CARTESIAN_POINT('Ctrl Pts',(14.3182869435397,-0.0163844490157649,
3.54237954232867));
#31345=CARTESIAN_POINT('Ctrl Pts',(14.3104155714898,-0.0918008565421096,
3.54507971943691));
#31346=CARTESIAN_POINT('Ctrl Pts',(14.3025441994398,-0.166535595070972,
3.56681902799889));
#31347=CARTESIAN_POINT('Ctrl Pts',(14.2946728273899,-0.231633314431234,
3.60499247969884));
#31348=CARTESIAN_POINT('Ctrl Pts',(14.2868014553399,-0.296731033791496,
3.64316593139879));
#31349=CARTESIAN_POINT('Ctrl Pts',(14.2789300832899,-0.352191733983158,
3.6977735262367));
#31350=CARTESIAN_POINT('Ctrl Pts',(14.27105871124,-0.391369643565407,3.76227171909014));
#31351=CARTESIAN_POINT('Ctrl Pts',(14.26318733919,-0.430547553147657,3.82676991194359));
#31352=CARTESIAN_POINT('Ctrl Pts',(14.2553159671401,-0.453442672120494,
3.90115870281258));
#31353=CARTESIAN_POINT('Ctrl Pts',(14.2474445950901,-0.457311513162664,
3.97652419590847));
#31354=CARTESIAN_POINT('Ctrl Pts',(14.2395732230402,-0.461180354204834,
4.05188968900435));
#31355=CARTESIAN_POINT('Ctrl Pts',(14.2317018509902,-0.446022917316338,
4.12823188432714));
#31356=CARTESIAN_POINT('Ctrl Pts',(14.2238304789403,-0.413655495130362,
4.19640281260034));
#31357=CARTESIAN_POINT('Ctrl Pts',(14.2159591068903,-0.381288072944386,
4.26457374087354));
#31358=CARTESIAN_POINT('Ctrl Pts',(14.2080877348403,-0.33171066546093,4.32457340209717));
#31359=CARTESIAN_POINT('Ctrl Pts',(14.2002163627904,-0.270864058094251,
4.36921212802613));
#31360=CARTESIAN_POINT('Ctrl Pts',(14.1923449907404,-0.210017450727571,
4.41385085395509));
#31361=CARTESIAN_POINT('Ctrl Pts',(14.1844736186905,-0.137901643477669,
4.44312864458938));
#31362=CARTESIAN_POINT('Ctrl Pts',(14.1766022466405,-0.0631581639595259,
4.45353718675995));
#31363=CARTESIAN_POINT('Ctrl Pts',(14.1744000672554,-0.0422471272657682,
4.45644919204336));
#31364=CARTESIAN_POINT('Ctrl Pts',(14.1721978878703,-0.021130418320356,
4.45788427006097));
#31365=CARTESIAN_POINT('Ctrl Pts',(14.1699957084852,-1.10604184835328E-5,
4.4578646218584));
#31366=CARTESIAN_POINT('Ctrl Pts',(14.2800042915148,1.11332528513013E-5,
4.45786561359635));
#31367=CARTESIAN_POINT('Ctrl Pts',(14.2857095446447,-0.0547030874695854,
4.45781418483069));
#31368=CARTESIAN_POINT('Ctrl Pts',(14.2914147977746,-0.109435272994953,
4.44799629651036));
#31369=CARTESIAN_POINT('Ctrl Pts',(14.2971200509045,-0.16065599949712,4.42880599334559));
#31370=CARTESIAN_POINT('Ctrl Pts',(14.3049914229545,-0.231323748287136,
4.40232968939868));
#31371=CARTESIAN_POINT('Ctrl Pts',(14.3128627950045,-0.295307463087888,
4.35801306922771));
#31372=CARTESIAN_POINT('Ctrl Pts',(14.3207341670544,-0.344940072567234,
4.30116652609615));
#31373=CARTESIAN_POINT('Ctrl Pts',(14.3286055391044,-0.394572682046581,
4.24431998296459));
#31374=CARTESIAN_POINT('Ctrl Pts',(14.3364769111543,-0.429854186204522,
4.17494351687244));
#31375=CARTESIAN_POINT('Ctrl Pts',(14.3443482832043,-0.446556856002091,
4.10135040434572));
#31376=CARTESIAN_POINT('Ctrl Pts',(14.3522196552542,-0.46325952579966,4.027757291819));
#31377=CARTESIAN_POINT('Ctrl Pts',(14.3600910273042,-0.461383361236856,
3.9499475328577));
#31378=CARTESIAN_POINT('Ctrl Pts',(14.3679623993541,-0.441153180262727,
3.87724495265939));
#31379=CARTESIAN_POINT('Ctrl Pts',(14.3758337714041,-0.420922999288597,
3.80454237246108));
#31380=CARTESIAN_POINT('Ctrl Pts',(14.383705143454,-0.382338801903142,3.73694697102576));
#31381=CARTESIAN_POINT('Ctrl Pts',(14.391576515504,-0.330024073856894,3.68255860260764));
#31382=CARTESIAN_POINT('Ctrl Pts',(14.399447887554,-0.277709345810648,3.62817023418952));
#31383=CARTESIAN_POINT('Ctrl Pts',(14.4073192596039,-0.21166408710361,3.58698889878861));
#31384=CARTESIAN_POINT('Ctrl Pts',(14.4151906316539,-0.139802400742051,
3.56394929325792));
#31385=CARTESIAN_POINT('Ctrl Pts',(14.4230620037038,-0.0679407143804897,
3.54090968772722));
#31386=CARTESIAN_POINT('Ctrl Pts',(14.4309333757538,0.00973739963559066,
3.53601181206673));
#31387=CARTESIAN_POINT('Ctrl Pts',(14.4388047478037,0.0839238909224197,
3.54984257127538));
#31388=CARTESIAN_POINT('Ctrl Pts',(14.4466761198537,0.158110382209248,3.56367333048403));
#31389=CARTESIAN_POINT('Ctrl Pts',(14.4545474919037,0.228805250766822,3.59623272456181));
#31390=CARTESIAN_POINT('Ctrl Pts',(14.4624188639536,0.287537237904754,3.64361921078484));
#31391=CARTESIAN_POINT('Ctrl Pts',(14.4702902360036,0.346269225042686,3.69100569700788));
#31392=CARTESIAN_POINT('Ctrl Pts',(14.4781616080535,0.393038330760977,3.75321927537615));
#31393=CARTESIAN_POINT('Ctrl Pts',(14.4860329801035,0.422240284179214,3.8228049873169));
#31394=CARTESIAN_POINT('Ctrl Pts',(14.4939043521534,0.451442237597453,3.89239069925764));
#31395=CARTESIAN_POINT('Ctrl Pts',(14.5017757242034,0.463077038715637,3.96934854477086));
#31396=CARTESIAN_POINT('Ctrl Pts',(14.5096470962533,0.45575050699275,4.04445678215295));
#31397=CARTESIAN_POINT('Ctrl Pts',(14.5175184683033,0.448423975269863,4.11956501953505));
#31398=CARTESIAN_POINT('Ctrl Pts',(14.5253898403532,0.422136110705906,4.19282364878603));
#31399=CARTESIAN_POINT('Ctrl Pts',(14.5332612124032,0.380036948171907,4.2554541996672));
#31400=CARTESIAN_POINT('Ctrl Pts',(14.5411325844532,0.337937785637909,4.31808475054837));
#31401=CARTESIAN_POINT('Ctrl Pts',(14.5490039565031,0.28002732513387,4.37008722305972));
#31402=CARTESIAN_POINT('Ctrl Pts',(14.5568753285531,0.213244889156206,4.40523023992844));
#31403=CARTESIAN_POINT('Ctrl Pts',(14.5645849828737,0.147834501639678,4.43965124177167));
#31404=CARTESIAN_POINT('Ctrl Pts',(14.5722946371942,0.0739129441497101,
4.45789842831743));
#31405=CARTESIAN_POINT('Ctrl Pts',(14.5800042915148,-1.58578451148518E-6,
4.45791318879952));
#31406=CARTESIAN_POINT('Origin',(12.5,0.,4.));
#31407=CARTESIAN_POINT('',(14.8800042915148,-1.01702808208336E-5,4.45785711824254));
#31408=CARTESIAN_POINT('',(14.7699957084852,8.6346448269735E-6,4.45789857801605));
#31409=CARTESIAN_POINT('',(12.5,-5.60735153159594E-17,4.457875));
#31410=CARTESIAN_POINT('Ctrl Pts',(14.7699957084852,8.6346448269735E-6,
4.45789857801605));
#31411=CARTESIAN_POINT('Ctrl Pts',(14.7689821891192,0.00972641784825355,
4.45790700998655));
#31412=CARTESIAN_POINT('Ctrl Pts',(14.7679686697532,0.01944367562558,4.45760386164098));
#31413=CARTESIAN_POINT('Ctrl Pts',(14.7669551503872,0.0291408329004781,
4.45698549795522));
#31414=CARTESIAN_POINT('Ctrl Pts',(14.7590837783372,0.104452598317788,4.45218305332902));
#31415=CARTESIAN_POINT('Ctrl Pts',(14.7512124062873,0.178551969979598,4.4283678943965));
#31416=CARTESIAN_POINT('Ctrl Pts',(14.7433410342373,0.242559732875008,4.38839375563686));
#31417=CARTESIAN_POINT('Ctrl Pts',(14.7354696621874,0.30656749577042,4.34841961687722));
#31418=CARTESIAN_POINT('Ctrl Pts',(14.7275982901374,0.360483649899433,4.29228649829047));
#31419=CARTESIAN_POINT('Ctrl Pts',(14.7197269180875,0.397847504376097,4.22672074611392));
#31420=CARTESIAN_POINT('Ctrl Pts',(14.7118555460375,0.435211358852761,4.16115499393738));
#31421=CARTESIAN_POINT('Ctrl Pts',(14.7039841739875,0.456022913677073,4.08615660817103));
#31422=CARTESIAN_POINT('Ctrl Pts',(14.6961128019376,0.457788351878884,4.01071253147039));
#31423=CARTESIAN_POINT('Ctrl Pts',(14.6882414298876,0.459553790080695,3.93526845476975));
#31424=CARTESIAN_POINT('Ctrl Pts',(14.6803700578377,0.442273111660005,3.85937868713481));
#31425=CARTESIAN_POINT('Ctrl Pts',(14.6724986857877,0.408017034045316,3.79213698410258));
#31426=CARTESIAN_POINT('Ctrl Pts',(14.6646273137378,0.373760956430627,3.72489528107034));
#31427=CARTESIAN_POINT('Ctrl Pts',(14.6567559416878,0.32252947962194,3.6663016426408));
#31428=CARTESIAN_POINT('Ctrl Pts',(14.6488845696379,0.260461593653079,3.6233772554918));
#31429=CARTESIAN_POINT('Ctrl Pts',(14.6410131975879,0.198393707684219,3.5804528683428));
#31430=CARTESIAN_POINT('Ctrl Pts',(14.6331418255379,0.125489412555185,3.55319773247434));
#31431=CARTESIAN_POINT('Ctrl Pts',(14.625270453488,0.0504847191830214,3.54487778940425));
#31432=CARTESIAN_POINT('Ctrl Pts',(14.617399081438,-0.0245199741891427,
3.53655784633416));
#31433=CARTESIAN_POINT('Ctrl Pts',(14.6095277093881,-0.101625065804437,
3.54717309606245));
#31434=CARTESIAN_POINT('Ctrl Pts',(14.6016563373381,-0.171591169681571,
3.57545152934398));
#31435=CARTESIAN_POINT('Ctrl Pts',(14.5937849652882,-0.241557273558703,
3.6037299626255));
#31436=CARTESIAN_POINT('Ctrl Pts',(14.5859135932382,-0.304384389697674,
3.64967157946028));
#31437=CARTESIAN_POINT('Ctrl Pts',(14.5780422211883,-0.352544040227279,
3.70777126570269));
#31438=CARTESIAN_POINT('Ctrl Pts',(14.5701708491383,-0.400703690756885,
3.7658709519451));
#31439=CARTESIAN_POINT('Ctrl Pts',(14.5622994770883,-0.434195875677124,
3.83612870759516));
#31440=CARTESIAN_POINT('Ctrl Pts',(14.5544281050384,-0.449007277354457,
3.91012565253846));
#31441=CARTESIAN_POINT('Ctrl Pts',(14.5465567329884,-0.46381867903179,3.98412259748177));
#31442=CARTESIAN_POINT('Ctrl Pts',(14.5386853609385,-0.459949297466218,
4.06185873171832));
#31443=CARTESIAN_POINT('Ctrl Pts',(14.5308139888885,-0.437862794771992,
4.13401905238929));
#31444=CARTESIAN_POINT('Ctrl Pts',(14.5229426168386,-0.415776292077766,
4.20617937306026));
#31445=CARTESIAN_POINT('Ctrl Pts',(14.5150712447886,-0.375472668254887,
4.27276388016565));
#31446=CARTESIAN_POINT('Ctrl Pts',(14.5071998727387,-0.321781445311454,
4.32579385338299));
#31447=CARTESIAN_POINT('Ctrl Pts',(14.4993285006887,-0.26809022236802,4.37882382660034));
#31448=CARTESIAN_POINT('Ctrl Pts',(14.4914571286387,-0.201011400304033,
4.41829926592964));
#31449=CARTESIAN_POINT('Ctrl Pts',(14.4835857565888,-0.128582932452519,
4.43948988945229));
#31450=CARTESIAN_POINT('Ctrl Pts',(14.4790557405542,-0.0868999680795747,
4.45168520479633));
#31451=CARTESIAN_POINT('Ctrl Pts',(14.4745257245197,-0.0434451672832877,
4.45782447382869));
#31452=CARTESIAN_POINT('Ctrl Pts',(14.4699957084852,4.96934848862042E-6,
4.4578413260902));
#31453=CARTESIAN_POINT('Ctrl Pts',(14.5800042915148,-1.58578451148518E-6,
4.45791318879952));
#31454=CARTESIAN_POINT('Ctrl Pts',(14.5801660092442,-0.00155201715944126,
4.45791349841543));
#31455=CARTESIAN_POINT('Ctrl Pts',(14.5803277269736,-0.00310244544229786,
4.45790578589721));
#31456=CARTESIAN_POINT('Ctrl Pts',(14.5804894447029,-0.0046527920161852,
4.45789003224535));
#31457=CARTESIAN_POINT('Ctrl Pts',(14.5883608167529,-0.0801136257596197,
4.45712324646747));
#31458=CARTESIAN_POINT('Ctrl Pts',(14.5962321888029,-0.155380881795201,
4.43730611368561));
#31459=CARTESIAN_POINT('Ctrl Pts',(14.6041035608528,-0.22143539919095,4.4008132908088));
#31460=CARTESIAN_POINT('Ctrl Pts',(14.6119749329028,-0.287489916586699,
4.36432046793199));
#31461=CARTESIAN_POINT('Ctrl Pts',(14.6198463049527,-0.344331695342615,
4.31115195496024));
#31462=CARTESIAN_POINT('Ctrl Pts',(14.6277176770027,-0.38514947146564,4.24767885402976));
#31463=CARTESIAN_POINT('Ctrl Pts',(14.6355890490526,-0.425967247588666,
4.18420575309928));
#31464=CARTESIAN_POINT('Ctrl Pts',(14.6434604211026,-0.4507610210788,4.11042806421008));
#31465=CARTESIAN_POINT('Ctrl Pts',(14.6513317931525,-0.45655979174196,4.03518645571321));
#31466=CARTESIAN_POINT('Ctrl Pts',(14.6592031652025,-0.462358562405121,
3.95994484721634));
#31467=CARTESIAN_POINT('Ctrl Pts',(14.6670745372524,-0.449162330241309,
3.8832393191118));
#31468=CARTESIAN_POINT('Ctrl Pts',(14.6749459093024,-0.41855237967279,3.81426137832517));
#31469=CARTESIAN_POINT('Ctrl Pts',(14.6828172813524,-0.387942429104271,
3.74528343753854));
#31470=CARTESIAN_POINT('Ctrl Pts',(14.6906886534023,-0.339918760131043,
3.68403308406983));
#31471=CARTESIAN_POINT('Ctrl Pts',(14.6985600254523,-0.280235976103336,
3.63784985464301));
#31472=CARTESIAN_POINT('Ctrl Pts',(14.7064313975022,-0.220553192075631,
3.5916666252162));
#31473=CARTESIAN_POINT('Ctrl Pts',(14.7143027695522,-0.149211292993445,
3.5605505198313));
#31474=CARTESIAN_POINT('Ctrl Pts',(14.7221741416021,-0.0747590701011626,
3.54823013427646));
#31475=CARTESIAN_POINT('Ctrl Pts',(14.7300455136521,-0.000306847208877067,
3.53590974872161));
#31476=CARTESIAN_POINT('Ctrl Pts',(14.737916885702,0.0772556994935079,3.54238508299684));
#31477=CARTESIAN_POINT('Ctrl Pts',(14.745788257752,0.148634367597872,3.5668802073009));
#31478=CARTESIAN_POINT('Ctrl Pts',(14.753659629802,0.220013035702235,3.59137533160497));
#31479=CARTESIAN_POINT('Ctrl Pts',(14.7615310018519,0.285207825208577,3.63389024593787));
#31480=CARTESIAN_POINT('Ctrl Pts',(14.7694023739019,0.336406544142474,3.68933045342307));
#31481=CARTESIAN_POINT('Ctrl Pts',(14.7772737459518,0.387605263076371,3.74477066090827));
#31482=CARTESIAN_POINT('Ctrl Pts',(14.7851451180018,0.424807911437823,3.81313616154577));
#31483=CARTESIAN_POINT('Ctrl Pts',(14.7930164900517,0.443556551112275,3.88623481973509));
#31484=CARTESIAN_POINT('Ctrl Pts',(14.8008878621017,0.462305190786727,3.9593334779244));
#31485=CARTESIAN_POINT('Ctrl Pts',(14.8087592341516,0.462599821774179,4.03716529366552));
#31486=CARTESIAN_POINT('Ctrl Pts',(14.8166306062016,0.444405141642572,4.11040380200553));
#31487=CARTESIAN_POINT('Ctrl Pts',(14.8245019782516,0.426210461510966,4.18364231034555));
#31488=CARTESIAN_POINT('Ctrl Pts',(14.8323733503015,0.389526470260302,4.25228751128446));
#31489=CARTESIAN_POINT('Ctrl Pts',(14.8402447223515,0.338748948932789,4.3081137476731));
#31490=CARTESIAN_POINT('Ctrl Pts',(14.8481160944014,0.287971427605278,4.36393998406173));
#31491=CARTESIAN_POINT('Ctrl Pts',(14.8559874664514,0.22310037620092,4.40694725590009));
#31492=CARTESIAN_POINT('Ctrl Pts',(14.8638588385013,0.151909206873508,4.43198208217373));
#31493=CARTESIAN_POINT('Ctrl Pts',(14.8692406561725,0.103234351881841,4.44909890368578));
#31494=CARTESIAN_POINT('Ctrl Pts',(14.8746224738437,0.0516050086776526,
4.45781408155485));
#31495=CARTESIAN_POINT('Ctrl Pts',(14.8800042915148,-1.01702808208336E-5,
4.45785711824254));
#31496=CARTESIAN_POINT('Origin',(12.5,0.,4.));
#31497=CARTESIAN_POINT('',(15.1,-5.60735153159594E-17,4.457875));
#31498=CARTESIAN_POINT('',(15.0699957084852,-1.05870731373636E-5,4.45788944868556));
#31499=CARTESIAN_POINT('',(12.5,-5.60735153159594E-17,4.457875));
#31500=CARTESIAN_POINT('',(15.1,-0.269165465906718,4.37040446485999));
#31501=CARTESIAN_POINT('Origin',(15.1,0.,4.));
#31502=CARTESIAN_POINT('Ctrl Pts',(15.1,-0.269173508333955,4.37043259773194));
#31503=CARTESIAN_POINT('Ctrl Pts',(15.0991842588284,-0.262849866117432,
4.37503549456412));
#31504=CARTESIAN_POINT('Ctrl Pts',(15.0983685176569,-0.256407545646713,
4.37947450812006));
#31505=CARTESIAN_POINT('Ctrl Pts',(15.0975527764853,-0.249853611926923,
4.38374199825787));
#31506=CARTESIAN_POINT('Ctrl Pts',(15.0896814044354,-0.186612411779406,
4.42492050409441));
#31507=CARTESIAN_POINT('Ctrl Pts',(15.0818100323854,-0.112978907049287,
4.45012847221118));
#31508=CARTESIAN_POINT('Ctrl Pts',(15.0739386603355,-0.0377721395608013,
4.45635245505497));
#31509=CARTESIAN_POINT('Ctrl Pts',(15.072624343052,-0.0252145379490987,
4.45739170058566));
#31510=CARTESIAN_POINT('Ctrl Pts',(15.0713100257686,-0.0126130730861363,
4.45790166433459));
#31511=CARTESIAN_POINT('Ctrl Pts',(15.0699957084852,-1.05870731373636E-5,
4.45788944868556));
#31512=CARTESIAN_POINT('Origin',(11.8752146997001,0.,4.));
#31513=CARTESIAN_POINT('',(14.9247853002999,-1.38824472118437E-5,4.62497559137666));
#31514=CARTESIAN_POINT('',(15.0252146997001,-1.44513692928093E-5,4.62501972247551));
#31515=CARTESIAN_POINT('',(11.8752146997001,-1.68747709936658E-14,4.625));
#31516=CARTESIAN_POINT('',(15.1,-0.624993681275899,4.00281040303151));
#31517=CARTESIAN_POINT('Ctrl Pts',(15.0252146997001,-1.44513692928189E-5,
4.62501972247551));
#31518=CARTESIAN_POINT('Ctrl Pts',(15.0265290169835,-0.017216861979444,
4.62503639685311));
#31519=CARTESIAN_POINT('Ctrl Pts',(15.0357147063169,-0.137433797398843,
4.62017138475037));
#31520=CARTESIAN_POINT('Ctrl Pts',(15.0527717677003,-0.355236031271534,
4.54560815721762));
#31521=CARTESIAN_POINT('Ctrl Pts',(15.0763858838501,-0.571652475026301,
4.31158258982903));
#31522=CARTESIAN_POINT('Ctrl Pts',(15.09212862795,-0.624530364890795,4.10584538053252));
#31523=CARTESIAN_POINT('Ctrl Pts',(15.1,-0.624993681275899,4.00281040303152));
#31524=CARTESIAN_POINT('',(15.1,0.314930721058197,3.46014479632612));
#31525=CARTESIAN_POINT('Origin',(15.1,0.,4.));
#31526=CARTESIAN_POINT('Ctrl Pts',(14.9247853002999,-1.38824472118368E-5,
4.62497559137666));
#31527=CARTESIAN_POINT('Ctrl Pts',(14.9272748546787,-0.0326052931943186,
4.62500276606431));
#31528=CARTESIAN_POINT('Ctrl Pts',(14.9376357811074,-0.168225686180582,
4.61457389311938));
#31529=CARTESIAN_POINT('Ctrl Pts',(14.9558680795861,-0.394527586443172,
4.517903766532));
#31530=CARTESIAN_POINT('Ctrl Pts',(14.979482195736,-0.593077772790822,4.26857965265179));
#31531=CARTESIAN_POINT('Ctrl Pts',(15.0030963118859,-0.649493436571599,
3.95488773069898));
#31532=CARTESIAN_POINT('Ctrl Pts',(15.0267104280357,-0.550252000240565,
3.65200904506483));
#31533=CARTESIAN_POINT('Ctrl Pts',(15.0503245441856,-0.319142060764588,
3.43252503194012));
#31534=CARTESIAN_POINT('Ctrl Pts',(15.0739386603355,-0.0115409051696555,
3.34904846156061));
#31535=CARTESIAN_POINT('Ctrl Pts',(15.0904971456069,0.20608092381284,3.39989411918499));
#31536=CARTESIAN_POINT('Ctrl Pts',(15.0991842588284,0.305720220830039,3.45471854406458));
#31537=CARTESIAN_POINT('Ctrl Pts',(15.1,0.314937815442301,3.46010549098218));
#31538=CARTESIAN_POINT('Origin',(11.8752146997001,0.,4.));
#31539=CARTESIAN_POINT('',(14.6247853002999,-2.16459804047719E-6,4.62505212776347));
#31540=CARTESIAN_POINT('',(14.7252146997001,1.17863019661874E-5,4.62503218402409));
#31541=CARTESIAN_POINT('',(11.8752146997001,-1.68747709936658E-14,4.625));
#31542=CARTESIAN_POINT('Ctrl Pts',(14.7252146997001,1.17863019662174E-5,
4.62503218402409));
#31543=CARTESIAN_POINT('Ctrl Pts',(14.7320725523841,-0.0897427467603322,
4.62495430540108));
#31544=CARTESIAN_POINT('Ctrl Pts',(14.746801777118,-0.282587126126967,4.58296482291278));
#31545=CARTESIAN_POINT('Ctrl Pts',(14.7694023739019,-0.520130285395982,
4.39158760667368));
#31546=CARTESIAN_POINT('Ctrl Pts',(14.7930164900517,-0.64367318065081,4.09778141619902));
#31547=CARTESIAN_POINT('Ctrl Pts',(14.8166306062016,-0.612955311082805,
3.78054123783642));
#31548=CARTESIAN_POINT('Ctrl Pts',(14.8402447223515,-0.435338447621071,
3.51589585985611));
#31549=CARTESIAN_POINT('Ctrl Pts',(14.8638588385013,-0.153389665944836,
3.36726945127358));
#31550=CARTESIAN_POINT('Ctrl Pts',(14.8874729546512,0.165319955489652,3.37028123293502));
#31551=CARTESIAN_POINT('Ctrl Pts',(14.9110870708011,0.444409630539555,3.52420969451069));
#31552=CARTESIAN_POINT('Ctrl Pts',(14.9347011869509,0.616993161964042,3.79216419995926));
#31553=CARTESIAN_POINT('Ctrl Pts',(14.9583153031008,0.641710593195818,4.10992889087348));
#31554=CARTESIAN_POINT('Ctrl Pts',(14.9819294192507,0.512636325700993,4.40134645341462));
#31555=CARTESIAN_POINT('Ctrl Pts',(15.0042292181171,0.274729866520086,4.58571614948967));
#31556=CARTESIAN_POINT('Ctrl Pts',(15.0186576449336,0.0858074045169303,
4.62493653494651));
#31557=CARTESIAN_POINT('Ctrl Pts',(15.0252146997001,-1.44513692928189E-5,
4.62501972247551));
#31558=CARTESIAN_POINT('Ctrl Pts',(14.6247853002999,-2.16459804049194E-6,
4.62505212776347));
#31559=CARTESIAN_POINT('Ctrl Pts',(14.6249470180292,-0.00211850554115318,
4.62505255038961));
#31560=CARTESIAN_POINT('Ctrl Pts',(14.6329801078086,-0.107244412024774,
4.62452960748548));
#31561=CARTESIAN_POINT('Ctrl Pts',(14.6488845696379,-0.314835022974042,
4.56987302880665));
#31562=CARTESIAN_POINT('Ctrl Pts',(14.6724986857877,-0.547602339746838,
4.35214775046202));
#31563=CARTESIAN_POINT('Ctrl Pts',(14.6961128019376,-0.649132943719538,
4.05002781234082));
#31564=CARTESIAN_POINT('Ctrl Pts',(14.7197269180875,-0.595094318970103,
3.73591836064326));
#31565=CARTESIAN_POINT('Ctrl Pts',(14.7433410342373,-0.398437197867616,
3.48509791236843));
#31566=CARTESIAN_POINT('Ctrl Pts',(14.7669551503872,-0.1062918289807,3.35767733339665));
#31567=CARTESIAN_POINT('Ctrl Pts',(14.7905692665371,0.211327117384507,3.38419385377023));
#31568=CARTESIAN_POINT('Ctrl Pts',(14.8141833826869,0.478300047385911,3.5582926020622));
#31569=CARTESIAN_POINT('Ctrl Pts',(14.8377974988368,0.630645044771057,3.83824960712979));
#31570=CARTESIAN_POINT('Ctrl Pts',(14.8614116149867,0.631851559871185,4.15697121131127));
#31571=CARTESIAN_POINT('Ctrl Pts',(14.8850257311365,0.481630465478622,4.4380735902585));
#31572=CARTESIAN_POINT('Ctrl Pts',(14.9061502929076,0.243989509668873,4.59562135563586));
#31573=CARTESIAN_POINT('Ctrl Pts',(14.9194034826287,0.0704409072858971,
4.62491684623921));
#31574=CARTESIAN_POINT('Ctrl Pts',(14.9247853002999,-1.38824472118368E-5,
4.62497559137666));
#31575=CARTESIAN_POINT('Origin',(11.8752146997001,0.,4.));
#31576=CARTESIAN_POINT('',(14.3247853002999,1.51969053300144E-5,4.6249871875462));
#31577=CARTESIAN_POINT('',(14.4252146997001,6.78316748347314E-6,4.62495403506715));
#31578=CARTESIAN_POINT('',(11.8752146997001,-1.68747709936658E-14,4.625));
#31579=CARTESIAN_POINT('Ctrl Pts',(14.4252146997001,6.78316748347826E-6,
4.62495403506715));
#31580=CARTESIAN_POINT('Ctrl Pts',(14.4297447157347,-0.0593027126443913,
4.62493103170719));
#31581=CARTESIAN_POINT('Ctrl Pts',(14.4421461038192,-0.221686029527806,
4.60198961095629));
#31582=CARTESIAN_POINT('Ctrl Pts',(14.4624188639536,-0.457506203155893,
4.46321101183598));
#31583=CARTESIAN_POINT('Ctrl Pts',(14.4860329801035,-0.622549707754089,
4.19054718257559));
#31584=CARTESIAN_POINT('Ctrl Pts',(14.5096470962533,-0.63839484111024,3.87221739454711));
#31585=CARTESIAN_POINT('Ctrl Pts',(14.5332612124032,-0.501244206711231,
3.58451159745434));
#31586=CARTESIAN_POINT('Ctrl Pts',(14.5568753285531,-0.243966908844842,
3.39638048838484));
#31587=CARTESIAN_POINT('Ctrl Pts',(14.5804894447029,0.0717787570654544,
3.35291099727801));
#31588=CARTESIAN_POINT('Ctrl Pts',(14.6041035608528,0.370322144162233,3.46452089026927));
#31589=CARTESIAN_POINT('Ctrl Pts',(14.6277176770027,0.580115251486915,3.70446207957941));
#31590=CARTESIAN_POINT('Ctrl Pts',(14.6513317931525,0.650879700384091,4.0152309888134));
#31591=CARTESIAN_POINT('Ctrl Pts',(14.6749459093024,0.565656298155129,4.32234968564526));
#31592=CARTESIAN_POINT('Ctrl Pts',(14.6985600254523,0.344869426209941,4.55221503612336));
#31593=CARTESIAN_POINT('Ctrl Pts',(14.7153162889182,0.129554394067723,4.62141618582314));
#31594=CARTESIAN_POINT('Ctrl Pts',(14.7242011803341,0.0132765736394338,
4.62504369367533));
#31595=CARTESIAN_POINT('Ctrl Pts',(14.7252146997001,1.17863019662174E-5,
4.62503218402409));
#31596=CARTESIAN_POINT('Ctrl Pts',(14.3247853002999,1.51969053300109E-5,
4.6249871875462));
#31597=CARTESIAN_POINT('Ctrl Pts',(14.3304905534298,-0.0746697890657793,
4.62491698721088));
#31598=CARTESIAN_POINT('Ctrl Pts',(14.3440671786096,-0.252453835406249,
4.59302599116618));
#31599=CARTESIAN_POINT('Ctrl Pts',(14.3655151758395,-0.490432948250941,
4.42819608115853));
#31600=CARTESIAN_POINT('Ctrl Pts',(14.3891292919893,-0.634910852255616,
4.14409916841427));
#31601=CARTESIAN_POINT('Ctrl Pts',(14.4127434081392,-0.627227950688033,
3.82546788683648));
#31602=CARTESIAN_POINT('Ctrl Pts',(14.4363575242891,-0.469225504392149,
3.54866444115539));
#31603=CARTESIAN_POINT('Ctrl Pts',(14.4599716404389,-0.198769899531221,
3.38002670405092));
#31604=CARTESIAN_POINT('Ctrl Pts',(14.4835857565888,0.11932229545683,3.35996988316441));
#31605=CARTESIAN_POINT('Ctrl Pts',(14.5071998727387,0.408818071695872,3.49330073524378));
#31606=CARTESIAN_POINT('Ctrl Pts',(14.5308139888885,0.600337751131954,3.74806559342675));
#31607=CARTESIAN_POINT('Ctrl Pts',(14.5544281050384,0.647982309355475,4.06320828594604));
#31608=CARTESIAN_POINT('Ctrl Pts',(14.5780422211883,0.540333396317157,4.36320267272319));
#31609=CARTESIAN_POINT('Ctrl Pts',(14.6014946196088,0.304813865567294,4.57469465218781));
#31610=CARTESIAN_POINT('Ctrl Pts',(14.6170756459793,0.100891269655612,4.62503197968527));
#31611=CARTESIAN_POINT('Ctrl Pts',(14.6247853002999,-2.16459804049194E-6,
4.62505212776347));
#31612=CARTESIAN_POINT('Origin',(11.8752146997001,0.,4.));
#31613=CARTESIAN_POINT('',(14.0247853002999,-6.3966029390794E-6,4.62495348172753));
#31614=CARTESIAN_POINT('',(14.1252146997001,-1.50974863142078E-5,4.62498583382255));
#31615=CARTESIAN_POINT('',(11.8752146997001,-1.68747709936658E-14,4.625));
#31616=CARTESIAN_POINT('Ctrl Pts',(14.1252146997001,-1.50974863141889E-5,
4.62498583382255));
#31617=CARTESIAN_POINT('Ctrl Pts',(14.1274168790852,-0.0288430498503269,
4.62501265364587));
#31618=CARTESIAN_POINT('Ctrl Pts',(14.1374904305203,-0.160695812902997,
4.61605202430223));
#31619=CARTESIAN_POINT('Ctrl Pts',(14.1554353540053,-0.385112282251534,
4.52494275637564));
#31620=CARTESIAN_POINT('Ctrl Pts',(14.1790494701552,-0.588131968915973,
4.27924389796604));
#31621=CARTESIAN_POINT('Ctrl Pts',(14.2026635863051,-0.65020173504413,3.96662229549764));
#31622=CARTESIAN_POINT('Ctrl Pts',(14.2262777024549,-0.556446129094758,
3.66199989226673));
#31623=CARTESIAN_POINT('Ctrl Pts',(14.2498918186048,-0.329334334698108,
3.43838156778717));
#31624=CARTESIAN_POINT('Ctrl Pts',(14.2735059347547,-0.0232952743833569,
3.34935901020328));
#31625=CARTESIAN_POINT('Ctrl Pts',(14.2971200509045,0.28832666060365,3.41626709515619));
#31626=CARTESIAN_POINT('Ctrl Pts',(14.3207341670544,0.530849104237583,3.62307083431711));
#31627=CARTESIAN_POINT('Ctrl Pts',(14.3443482832043,0.646149864620809,3.92020827196535));
#31628=CARTESIAN_POINT('Ctrl Pts',(14.3679623993541,0.606596311879891,4.2364683526943));
#31629=CARTESIAN_POINT('Ctrl Pts',(14.391576515504,0.42166773027486,4.49605714656388));
#31630=CARTESIAN_POINT('Ctrl Pts',(14.4106606156193,0.190545343529355,4.60977018898031));
#31631=CARTESIAN_POINT('Ctrl Pts',(14.4218733436847,0.0437536792250838,
4.62497100242767));
#31632=CARTESIAN_POINT('Ctrl Pts',(14.4252146997001,6.78316748347826E-6,
4.62495403506715));
#31633=CARTESIAN_POINT('Ctrl Pts',(14.0247853002999,-6.39660293913491E-6,
4.62495348172753));
#31634=CARTESIAN_POINT('Ctrl Pts',(14.0281627167804,-0.0442255271350925,
4.62496963662755));
#31635=CARTESIAN_POINT('Ctrl Pts',(14.0394115053108,-0.191490205391595,
4.6095527480466));
#31636=CARTESIAN_POINT('Ctrl Pts',(14.0585316658912,-0.422790583021024,
4.49510047824495));
#31637=CARTESIAN_POINT('Ctrl Pts',(14.0821457820411,-0.60713052675338,4.23509335195577));
#31638=CARTESIAN_POINT('Ctrl Pts',(14.1057598981909,-0.645967413308333,
3.91874446730605));
#31639=CARTESIAN_POINT('Ctrl Pts',(14.1293740143408,-0.529993712466286,
3.62186903671368));
#31640=CARTESIAN_POINT('Ctrl Pts',(14.1529881304907,-0.287003328966194,
3.41561532377041));
#31641=CARTESIAN_POINT('Ctrl Pts',(14.1766022466405,0.0247694002478971,
3.34941346658496));
#31642=CARTESIAN_POINT('Ctrl Pts',(14.2002163627904,0.330605970264406,3.43912920108534));
#31643=CARTESIAN_POINT('Ctrl Pts',(14.2238304789403,0.557210518047066,3.66326152695696));
#31644=CARTESIAN_POINT('Ctrl Pts',(14.2474445950901,0.650275686248857,3.96809557204375));
#31645=CARTESIAN_POINT('Ctrl Pts',(14.27105871124,0.587497759452106,4.28057573538778));
#31646=CARTESIAN_POINT('Ctrl Pts',(14.2946728273899,0.383921904832036,4.52581397056352));
#31647=CARTESIAN_POINT('Ctrl Pts',(14.3125816904098,0.159750963363977,4.61623247111552));
#31648=CARTESIAN_POINT('Ctrl Pts',(14.3226191813798,0.0283709170587055,
4.62501384057475));
#31649=CARTESIAN_POINT('Ctrl Pts',(14.3247853002999,1.51969053300109E-5,
4.6249871875462));
#31650=CARTESIAN_POINT('Origin',(11.8752146997001,0.,4.));
#31651=CARTESIAN_POINT('',(13.7247853002999,-1.20831421157597E-5,4.62503091248755));
#31652=CARTESIAN_POINT('',(13.8252146997001,1.68461488569462E-6,4.62505238998457));
#31653=CARTESIAN_POINT('',(11.8752146997001,-1.68747709936658E-14,4.625));
#31654=CARTESIAN_POINT('Ctrl Pts',(13.8252146997001,1.68461488569581E-6,
4.62505238998457));
#31655=CARTESIAN_POINT('Ctrl Pts',(13.8329604144858,-0.101363538932993,
4.62503644193381));
#31656=CARTESIAN_POINT('Ctrl Pts',(13.8485775013214,-0.305753798836605,
4.57432856173903));
#31657=CARTESIAN_POINT('Ctrl Pts',(13.8720659602069,-0.541154937947787,
4.36197748624323));
#31658=CARTESIAN_POINT('Ctrl Pts',(13.8956800763568,-0.648123865072376,
4.06173996222779));
#31659=CARTESIAN_POINT('Ctrl Pts',(13.9192941925067,-0.599765396122921,
3.74670602647169));
#31660=CARTESIAN_POINT('Ctrl Pts',(13.9429083086565,-0.407668974822819,
3.49237575473668));
#31661=CARTESIAN_POINT('Ctrl Pts',(13.9665224248064,-0.117871845784803,
3.35970116712309));
#31662=CARTESIAN_POINT('Ctrl Pts',(13.9901365409563,0.200174091641329,3.38047865214521));
#31663=CARTESIAN_POINT('Ctrl Pts',(14.0137506571061,0.470246914526057,3.54972874087838));
#31664=CARTESIAN_POINT('Ctrl Pts',(14.037364773256,0.627621790796785,3.82688947135059));
#31665=CARTESIAN_POINT('Ctrl Pts',(14.0609788894059,0.634582735815489,4.14553734509456));
#31666=CARTESIAN_POINT('Ctrl Pts',(14.0845930055557,0.489461510650943,4.42930618095194));
#31667=CARTESIAN_POINT('Ctrl Pts',(14.1060049423205,0.251510284961593,4.59332024860173));
#31668=CARTESIAN_POINT('Ctrl Pts',(14.1195455070353,0.074198300926532,4.62491679006221));
#31669=CARTESIAN_POINT('Ctrl Pts',(14.1252146997001,-1.50974863141889E-5,
4.62498583382255));
#31670=CARTESIAN_POINT('Ctrl Pts',(13.7247853002999,-1.20831421156938E-5,
4.62503091248755));
#31671=CARTESIAN_POINT('Ctrl Pts',(13.7258348801309,-0.013748904810447,
4.62504304225186));
#31672=CARTESIAN_POINT('Ctrl Pts',(13.734755832012,-0.130498998332177,4.62127102305724));
#31673=CARTESIAN_POINT('Ctrl Pts',(13.7515481559429,-0.346119716157775,
4.55143222859795));
#31674=CARTESIAN_POINT('Ctrl Pts',(13.7751622720928,-0.566385203513325,
4.32106722332061));
#31675=CARTESIAN_POINT('Ctrl Pts',(13.7987763882427,-0.650912534047929,
4.01375622291695));
#31676=CARTESIAN_POINT('Ctrl Pts',(13.8223905043925,-0.57944414457563,3.70314844792952));
#31677=CARTESIAN_POINT('Ctrl Pts',(13.8460046205424,-0.369107932149097,
3.46368321387984));
#31678=CARTESIAN_POINT('Ctrl Pts',(13.8696187366923,-0.0703124342978696,
3.35275003110641));
#31679=CARTESIAN_POINT('Ctrl Pts',(13.8932328528421,0.245333927901481,3.3969348091043));
#31680=CARTESIAN_POINT('Ctrl Pts',(13.916846968992,0.502184306426786,3.58564835824111));
#31681=CARTESIAN_POINT('Ctrl Pts',(13.9404610851419,0.638682720042094,3.87366416276737));
#31682=CARTESIAN_POINT('Ctrl Pts',(13.9640752012917,0.62211637371287,4.19195723015293));
#31683=CARTESIAN_POINT('Ctrl Pts',(13.9876893174416,0.456455507660852,4.46424641105313));
#31684=CARTESIAN_POINT('Ctrl Pts',(14.007926017111,0.220741531225703,4.60224444133776));
#31685=CARTESIAN_POINT('Ctrl Pts',(14.0202913447304,0.058831122868106,4.62493198618401));
#31686=CARTESIAN_POINT('Ctrl Pts',(14.0247853002999,-6.39660293913491E-6,
4.62495348172753));
#31687=CARTESIAN_POINT('Origin',(11.8752146997001,0.,4.));
#31688=CARTESIAN_POINT('',(13.4247853002999,1.36962628664028E-5,4.62502243215823));
#31689=CARTESIAN_POINT('',(13.5252146997001,1.40828270379035E-5,4.62497680637469));
#31690=CARTESIAN_POINT('',(11.8752146997001,-1.68747709936658E-14,4.625));
#31691=CARTESIAN_POINT('Ctrl Pts',(13.5252146997001,1.4082827037902E-5,
4.62497680637469));
#31692=CARTESIAN_POINT('Ctrl Pts',(13.5306325778363,-0.0709123884867814,
4.62491668074428));
#31693=CARTESIAN_POINT('Ctrl Pts',(13.5439218280225,-0.244933372371362,
4.59533688876844));
#31694=CARTESIAN_POINT('Ctrl Pts',(13.5650824502587,-0.482621788093898,
4.43698120905743));
#31695=CARTESIAN_POINT('Ctrl Pts',(13.5886965664085,-0.632205603168059,
4.15553919999523));
#31696=CARTESIAN_POINT('Ctrl Pts',(13.6123106825584,-0.630276944445953,
3.83682113889318));
#31697=CARTESIAN_POINT('Ctrl Pts',(13.6359247987083,-0.477298028416376,
3.55721002779864));
#31698=CARTESIAN_POINT('Ctrl Pts',(13.6595389148582,-0.209931317243796,
3.38371661595291));
#31699=CARTESIAN_POINT('Ctrl Pts',(13.683153031008,0.107746895509167,3.35791980725116));
#31700=CARTESIAN_POINT('Ctrl Pts',(13.7067671471579,0.399602814690774,3.48600198647908));
#31701=CARTESIAN_POINT('Ctrl Pts',(13.7303812633077,0.59569113756138,3.73726736776131));
#31702=CARTESIAN_POINT('Ctrl Pts',(13.7539953794576,0.649017932507905,4.05149845333026));
#31703=CARTESIAN_POINT('Ctrl Pts',(13.7776094956075,0.546803061895555,4.35338757606046));
#31704=CARTESIAN_POINT('Ctrl Pts',(13.8012236117573,0.313543031018869,4.57058490613733));
#31705=CARTESIAN_POINT('Ctrl Pts',(13.8170920131216,0.106300066848774,4.6246481407235));
#31706=CARTESIAN_POINT('Ctrl Pts',(13.8250890424358,0.00164611344283092,
4.62505264870678));
#31707=CARTESIAN_POINT('Ctrl Pts',(13.8252146997001,1.68461488569581E-6,
4.62505238998457));
#31708=CARTESIAN_POINT('Ctrl Pts',(13.4247853002999,1.36962628664097E-5,
4.62502243215823));
#31709=CARTESIAN_POINT('Ctrl Pts',(13.4313784155315,-0.086279884022628,
4.62493973056585));
#31710=CARTESIAN_POINT('Ctrl Pts',(13.445842902813,-0.275670893367246,4.58538934244717));
#31711=CARTESIAN_POINT('Ctrl Pts',(13.4681787621445,-0.513544980480383,
4.40018484937968));
#31712=CARTESIAN_POINT('Ctrl Pts',(13.4917928782944,-0.64195771209056,4.10847422061066));
#31713=CARTESIAN_POINT('Ctrl Pts',(13.5154069944443,-0.616520809113462,
3.79076698974655));
#31714=CARTESIAN_POINT('Ctrl Pts',(13.5390211105941,-0.443330402422436,
3.52320390633144));
#31715=CARTESIAN_POINT('Ctrl Pts',(13.562635226744,-0.163892778617988,3.36990832590288));
#31716=CARTESIAN_POINT('Ctrl Pts',(13.5862493428939,0.154822890495328,3.36761860145296));
#31717=CARTESIAN_POINT('Ctrl Pts',(13.6098634590437,0.43643417612693,3.51688348138565));
#31718=CARTESIAN_POINT('Ctrl Pts',(13.6334775751936,0.613450973283793,3.78193059814177));
#31719=CARTESIAN_POINT('Ctrl Pts',(13.6570916913435,0.643449974253473,4.09923956510808));
#31720=CARTESIAN_POINT('Ctrl Pts',(13.6807058074933,0.519241709620395,4.39276507945606));
#31721=CARTESIAN_POINT('Ctrl Pts',(13.7032703438121,0.281645253009076,4.58329909926801));
#31722=CARTESIAN_POINT('Ctrl Pts',(13.717963508081,0.0892710189108511,4.62495207452848));
#31723=CARTESIAN_POINT('Ctrl Pts',(13.7247853002999,-1.20831421156938E-5,
4.62503091248755));
#31724=CARTESIAN_POINT('Origin',(11.8752146997001,0.,4.));
#31725=CARTESIAN_POINT('',(13.1247853002999,3.84888821539087E-6,4.62495078081483));
#31726=CARTESIAN_POINT('',(13.2252146997001,-9.32440196476731E-6,4.62495874418382));
#31727=CARTESIAN_POINT('',(11.8752146997001,-1.68747709936658E-14,4.625));
#31728=CARTESIAN_POINT('Ctrl Pts',(13.2252146997001,-9.32440196474427E-6,
4.62495874418382));
#31729=CARTESIAN_POINT('Ctrl Pts',(13.2283047411869,-0.040464997295585,
4.62498052751194));
#31730=CARTESIAN_POINT('Ctrl Pts',(13.2392661547237,-0.18396024524725,4.61125364372682));
#31731=CARTESIAN_POINT('Ctrl Pts',(13.2580989403104,-0.413782468289504,
4.50265339583901));
#31732=CARTESIAN_POINT('Ctrl Pts',(13.2817130564603,-0.602786876612853,
4.24601696851145));
#31733=CARTESIAN_POINT('Ctrl Pts',(13.3053271726101,-0.647329213752593,
3.9304208620728));
#31734=CARTESIAN_POINT('Ctrl Pts',(13.32894128876,-0.536734598538914,3.6314998804023));
#31735=CARTESIAN_POINT('Ctrl Pts',(13.3525554049099,-0.297507800394296,
3.42089251764738));
#31736=CARTESIAN_POINT('Ctrl Pts',(13.3761695210598,0.0130188131672444,
3.34907229440132));
#31737=CARTESIAN_POINT('Ctrl Pts',(13.3997836372096,0.320425377524893,3.43325142712992));
#31738=CARTESIAN_POINT('Ctrl Pts',(13.4233977533595,0.551039769569266,3.65325580067535));
#31739=CARTESIAN_POINT('Ctrl Pts',(13.4470118695093,0.649593644862141,3.95635983539258));
#31740=CARTESIAN_POINT('Ctrl Pts',(13.4706259856592,0.592467881122722,4.26992253935193));
#31741=CARTESIAN_POINT('Ctrl Pts',(13.4942401018091,0.393353065302923,4.5187964277335));
#31742=CARTESIAN_POINT('Ctrl Pts',(13.5124363398227,0.1672808180195,4.61476328251587));
#31743=CARTESIAN_POINT('Ctrl Pts',(13.5227612057864,0.0321332374692893,
4.62500403435298));
#31744=CARTESIAN_POINT('Ctrl Pts',(13.5252146997001,1.4082827037902E-5,
4.62497680637469));
#31745=CARTESIAN_POINT('Ctrl Pts',(13.1247853002999,3.84888821536311E-6,
4.62495078081483));
#31746=CARTESIAN_POINT('Ctrl Pts',(13.1290505788821,-0.0558403875021823,
4.6249385719914));
#31747=CARTESIAN_POINT('Ctrl Pts',(13.1411872295142,-0.214751600407627,
4.60383286368317));
#31748=CARTESIAN_POINT('Ctrl Pts',(13.1611952521963,-0.449738236712957,
4.47075670902068));
#31749=CARTESIAN_POINT('Ctrl Pts',(13.1848093683461,-0.619294173608025,
4.2008758003961));
#31750=CARTESIAN_POINT('Ctrl Pts',(13.208423484496,-0.64043195068177,3.88285360784221));
#31751=CARTESIAN_POINT('Ctrl Pts',(13.2320376006459,-0.508085752511173,
3.59290636366459));
#31752=CARTESIAN_POINT('Ctrl Pts',(13.2556517167957,-0.253973266794505,
3.40052194335125));
#31753=CARTESIAN_POINT('Ctrl Pts',(13.2792658329456,0.0610056803032868,
3.3518066124833));
#31754=CARTESIAN_POINT('Ctrl Pts',(13.3028799490955,0.361364191435218,3.45843533922715));
#31755=CARTESIAN_POINT('Ctrl Pts',(13.3264940652453,0.575119258511334,3.69485380694));
#31756=CARTESIAN_POINT('Ctrl Pts',(13.3501081813952,0.65104299168552,4.00440268404554));
#31757=CARTESIAN_POINT('Ctrl Pts',(13.3737222975451,0.570939739771795,4.31289642727099));
#31758=CARTESIAN_POINT('Ctrl Pts',(13.3973364136949,0.354006804717113,4.54640236352309));
#31759=CARTESIAN_POINT('Ctrl Pts',(13.4143574146132,0.136489422610972,4.62032507485564));
#31760=CARTESIAN_POINT('Ctrl Pts',(13.4235070434815,0.0167440814458925,
4.62503846613771));
#31761=CARTESIAN_POINT('Ctrl Pts',(13.4247853002999,1.36962628664097E-5,
4.62502243215823));
#31762=CARTESIAN_POINT('Origin',(11.8752146997001,0.,4.));
#31763=CARTESIAN_POINT('',(12.8247853002999,-1.55438223423121E-5,4.62499607812274));
#31764=CARTESIAN_POINT('',(12.9252146997001,-9.4222586321007E-6,4.62504029123831));
#31765=CARTESIAN_POINT('',(11.8752146997001,-1.68747709936658E-14,4.625));
#31766=CARTESIAN_POINT('Ctrl Pts',(12.9252146997001,-9.42225863212465E-6,
4.62504029123832));
#31767=CARTESIAN_POINT('Ctrl Pts',(12.9259769045375,-0.00998466834883174,
4.6250476064301));
#31768=CARTESIAN_POINT('Ctrl Pts',(12.9346104814248,-0.122971475467856,
4.62239759066569));
#31769=CARTESIAN_POINT('Ctrl Pts',(12.9511154303622,-0.336107011072318,
4.55759164674784));
#31770=CARTESIAN_POINT('Ctrl Pts',(12.974729546512,-0.56049590900091,4.33124115596169));
#31771=CARTESIAN_POINT('Ctrl Pts',(12.9983436626619,-0.650558060547343,
4.02550641626558));
#31772=CARTESIAN_POINT('Ctrl Pts',(13.0219577788117,-0.584709444123524,
3.71365888635357));
#31773=CARTESIAN_POINT('Ctrl Pts',(13.0455718949616,-0.378731139057797,
3.47043499764384));
#31774=CARTESIAN_POINT('Ctrl Pts',(13.0691860111115,-0.0819872800401352,
3.35412504823007));
#31775=CARTESIAN_POINT('Ctrl Pts',(13.0928001272613,0.234405401379786,3.39260352716186));
#31776=CARTESIAN_POINT('Ctrl Pts',(13.1164142434112,0.494621196584012,3.57664879910166));
#31777=CARTESIAN_POINT('Ctrl Pts',(13.1400283595611,0.636297578801308,3.86215313342763));
#31778=CARTESIAN_POINT('Ctrl Pts',(13.1636424757109,0.625480816776257,4.18069342892634));
#31779=CARTESIAN_POINT('Ctrl Pts',(13.1872565918608,0.464763222827219,4.45592928631477));
#31780=CARTESIAN_POINT('Ctrl Pts',(13.2077806665239,0.228267895462889,4.60018049807294));
#31781=CARTESIAN_POINT('Ctrl Pts',(13.220433369137,0.0625891701764018,4.62492503806923));
#31782=CARTESIAN_POINT('Ctrl Pts',(13.2252146997001,-9.32440196474427E-6,
4.62495874418382));
#31783=CARTESIAN_POINT('Ctrl Pts',(12.8247853002999,-1.55438223423052E-5,
4.62499607812274));
#31784=CARTESIAN_POINT('Ctrl Pts',(12.8267227422326,-0.0253767156259869,
4.62502109614712));
#31785=CARTESIAN_POINT('Ctrl Pts',(12.8365315562153,-0.153759343851268,
4.61735081595804));
#31786=CARTESIAN_POINT('Ctrl Pts',(12.854211742248,-0.376327535803878,4.5312757721487));
#31787=CARTESIAN_POINT('Ctrl Pts',(12.8778258583979,-0.583405888470749,
4.28898776831928));
#31788=CARTESIAN_POINT('Ctrl Pts',(12.9014399745477,-0.650666957548692,
3.97744183415536));
#31789=CARTESIAN_POINT('Ctrl Pts',(12.9250540906976,-0.561991161265395,
3.67130212143154));
#31790=CARTESIAN_POINT('Ctrl Pts',(12.9486682068475,-0.338630270727757,
3.44393714350224));
#31791=CARTESIAN_POINT('Ctrl Pts',(12.9722823229973,-0.0341142786054444,
3.34983650006563));
#31792=CARTESIAN_POINT('Ctrl Pts',(12.9958964391472,0.278577437919422,3.41155206540036));
#31793=CARTESIAN_POINT('Ctrl Pts',(13.0195105552971,0.524506132150044,3.61429327464512));
#31794=CARTESIAN_POINT('Ctrl Pts',(13.0431246714469,0.644733280558021,3.90947178565704));
#31795=CARTESIAN_POINT('Ctrl Pts',(13.0667387875968,0.61044561006836,4.22634601343335));
#31796=CARTESIAN_POINT('Ctrl Pts',(13.0903529037467,0.429860399609997,4.4889748434194));
#31797=CARTESIAN_POINT('Ctrl Pts',(13.1097017413144,0.197481915229314,4.60814700801091));
#31798=CARTESIAN_POINT('Ctrl Pts',(13.1211792068321,0.0472175377905832,
4.6249611028038));
#31799=CARTESIAN_POINT('Ctrl Pts',(13.1247853002999,3.84888821536311E-6,
4.62495078081483));
#31800=CARTESIAN_POINT('Origin',(11.8752146997001,0.,4.));
#31801=CARTESIAN_POINT('',(12.5247853002999,3.80998376854277E-6,4.62503871776264));
#31802=CARTESIAN_POINT('',(12.6252146997001,1.49489494596481E-5,4.6250110476872));
#31803=CARTESIAN_POINT('',(11.8752146997001,-1.68747709936658E-14,4.625));
#31804=CARTESIAN_POINT('',(12.5,0.310062960217711,4.54266560670548));
#31805=CARTESIAN_POINT('Ctrl Pts',(12.5,0.310062960217722,4.54266560670548));
#31806=CARTESIAN_POINT('Ctrl Pts',(12.50787137205,0.220600394030941,4.59378185169648));
#31807=CARTESIAN_POINT('Ctrl Pts',(12.5161331388166,0.113220056708515,4.6237347594226));
#31808=CARTESIAN_POINT('Ctrl Pts',(12.5243949055832,0.00511234815255113,
4.6250406321328));
#31809=CARTESIAN_POINT('Ctrl Pts',(12.5247853002999,3.80998376856706E-6,
4.62503871776264));
#31810=CARTESIAN_POINT('',(12.5,0.310062960217774,3.45733439329455));
#31811=CARTESIAN_POINT('Origin',(12.5,0.,4.));
#31812=CARTESIAN_POINT('Ctrl Pts',(12.5,0.310093463203755,3.45730861053195));
#31813=CARTESIAN_POINT('Ctrl Pts',(12.5008157411716,0.319367492808711,3.46259780682489));
#31814=CARTESIAN_POINT('Ctrl Pts',(12.5095028543931,0.416666480413896,3.52147574364868));
#31815=CARTESIAN_POINT('Ctrl Pts',(12.5260613396645,0.569511032758309,3.68451895614546));
#31816=CARTESIAN_POINT('Ctrl Pts',(12.5496754558144,0.651018771792273,3.99264764559437));
#31817=CARTESIAN_POINT('Ctrl Pts',(12.5732895719643,0.576495013506714,4.3025367374363));
#31818=CARTESIAN_POINT('Ctrl Pts',(12.5969036881141,0.363815091701307,4.53992168461618));
#31819=CARTESIAN_POINT('Ctrl Pts',(12.6142120640261,0.144017971622128,4.61907377583531));
#31820=CARTESIAN_POINT('Ctrl Pts',(12.6236490678881,0.0205077016108913,
4.62503160004571));
#31821=CARTESIAN_POINT('Ctrl Pts',(12.6252146997001,1.49489494596471E-5,
4.6250110476872));
#31822=CARTESIAN_POINT('Origin',(11.8752146997001,0.,4.));
#31823=CARTESIAN_POINT('Ctrl Pts',(12.6252146997001,1.49489494596471E-5,
4.6250110476872));
#31824=CARTESIAN_POINT('Ctrl Pts',(12.631520439938,-0.0825216819810338,
4.62492827098767));
#31825=CARTESIAN_POINT('Ctrl Pts',(12.6456975522259,-0.268159494659544,
4.5879440580038));
#31826=CARTESIAN_POINT('Ctrl Pts',(12.6677460365637,-0.506235857616531,
4.40939182910775));
#31827=CARTESIAN_POINT('Ctrl Pts',(12.6913601527136,-0.639894509617229,
4.12004729681268));
#31828=CARTESIAN_POINT('Ctrl Pts',(12.7149742688635,-0.620198095551099,
3.8019325752266));
#31829=CARTESIAN_POINT('Ctrl Pts',(12.7385883850133,-0.451866840211785,
3.53128609963859));
#31830=CARTESIAN_POINT('Ctrl Pts',(12.7622025011632,-0.17524257447904,3.37297016902465));
#31831=CARTESIAN_POINT('Ctrl Pts',(12.7858166173131,0.143379805101228,3.36492630429559));
#31832=CARTESIAN_POINT('Ctrl Pts',(12.809430733463,0.42764021116234,3.50908227080648));
#31833=CARTESIAN_POINT('Ctrl Pts',(12.8330448496128,0.609413666055986,3.77089008898231));
#31834=CARTESIAN_POINT('Ctrl Pts',(12.8566589657627,0.645136892431096,4.08760569204938));
#31835=CARTESIAN_POINT('Ctrl Pts',(12.8802730819125,0.526248572038732,4.38332598125533));
#31836=CARTESIAN_POINT('Ctrl Pts',(12.903124993225,0.289149347937084,4.5805996458561));
#31837=CARTESIAN_POINT('Ctrl Pts',(12.9181055324875,0.0930307802739178,
4.62497206165088));
#31838=CARTESIAN_POINT('Ctrl Pts',(12.9252146997001,-9.42225863212465E-6,
4.62504029123832));
#31839=CARTESIAN_POINT('Ctrl Pts',(12.5247853002999,3.80998376856706E-6,
4.62503871776264));
#31840=CARTESIAN_POINT('Ctrl Pts',(12.5322662776332,-0.0978890574527522,
4.62500203345524));
#31841=CARTESIAN_POINT('Ctrl Pts',(12.5476186270164,-0.298862923743373,
4.57698368148067));
#31842=CARTESIAN_POINT('Ctrl Pts',(12.5708423484496,-0.535054221536356,
4.37092866956447));
#31843=CARTESIAN_POINT('Ctrl Pts',(12.5944564645995,-0.647009713430093,
4.07251155115386));
#31844=CARTESIAN_POINT('Ctrl Pts',(12.6180705807493,-0.603894380709874,
3.75671714932517));
#31845=CARTESIAN_POINT('Ctrl Pts',(12.6416846968992,-0.416056506175611,
3.49922677321964));
#31846=CARTESIAN_POINT('Ctrl Pts',(12.6652988130491,-0.128505496873939,
3.36175035317655));
#31847=CARTESIAN_POINT('Ctrl Pts',(12.6889129291989,0.189841674427298,3.37723482234205));
#31848=CARTESIAN_POINT('Ctrl Pts',(12.7125270453488,0.462692468193658,3.54196933898577));
#31849=CARTESIAN_POINT('Ctrl Pts',(12.7361411614987,0.624655556881011,3.81647407445394));
#31850=CARTESIAN_POINT('Ctrl Pts',(12.7597552776485,0.636915702199809,4.13496208375113));
#31851=CARTESIAN_POINT('Ctrl Pts',(12.7833693937984,0.496534514683115,4.42110548633398));
#31852=CARTESIAN_POINT('Ctrl Pts',(12.8050460680155,0.258436396781676,4.5911312751119));
#31853=CARTESIAN_POINT('Ctrl Pts',(12.8188513701827,0.0776597756952025,
4.62491945378327));
#31854=CARTESIAN_POINT('Ctrl Pts',(12.8247853002999,-1.55438223423052E-5,
4.62499607812274));
#31855=CARTESIAN_POINT('Ctrl Pts',(12.5,-0.186196943290592,3.58169363627332));
#31856=CARTESIAN_POINT('Ctrl Pts',(12.50787137205,-0.117235947257613,3.55099764935784));
#31857=CARTESIAN_POINT('Ctrl Pts',(12.5236141161499,0.0360970477778841,
3.52440632583991));
#31858=CARTESIAN_POINT('Ctrl Pts',(12.5472282322997,0.257537368848111,3.59853698535937));
#31859=CARTESIAN_POINT('Ctrl Pts',(12.5708423484496,0.417223782598737,3.76887858727216));
#31860=CARTESIAN_POINT('Ctrl Pts',(12.5944564645995,0.476936352215019,3.99461366516243));
#31861=CARTESIAN_POINT('Ctrl Pts',(12.6180705807493,0.422340246895018,4.22163841384584));
#31862=CARTESIAN_POINT('Ctrl Pts',(12.6416846968992,0.266530936180377,4.39554662614981));
#31863=CARTESIAN_POINT('Ctrl Pts',(12.6652988130491,0.0468439715927196,
4.47465904879863));
#31864=CARTESIAN_POINT('Ctrl Pts',(12.6889129291989,-0.184068700558194,
4.44001626345752));
#31865=CARTESIAN_POINT('Ctrl Pts',(12.7125270453488,-0.37086838928987,4.29992045400434));
#31866=CARTESIAN_POINT('Ctrl Pts',(12.7361411614987,-0.468786717745582,
4.08794664964497));
#31867=CARTESIAN_POINT('Ctrl Pts',(12.7597552776485,-0.454357124800734,
3.85489580461101));
#31868=CARTESIAN_POINT('Ctrl Pts',(12.7833693937984,-0.331037647139153,
3.65662019659523));
#31869=CARTESIAN_POINT('Ctrl Pts',(12.8069835099483,-0.128382710063344,
3.54063794582746));
#31870=CARTESIAN_POINT('Ctrl Pts',(12.8305976260981,0.10504004521716,3.53474501052695));
#31871=CARTESIAN_POINT('Ctrl Pts',(12.854211742248,0.31328921869753,3.64035367159283));
#31872=CARTESIAN_POINT('Ctrl Pts',(12.8778258583979,0.446456451752615,3.83215407918844));
#31873=CARTESIAN_POINT('Ctrl Pts',(12.9014399745477,0.47262728739502,4.06417992999538));
#31874=CARTESIAN_POINT('Ctrl Pts',(12.9250540906976,0.385529703875575,4.28082461386765));
#31875=CARTESIAN_POINT('Ctrl Pts',(12.9486682068475,0.206037242841946,4.43016772408018));
#31876=CARTESIAN_POINT('Ctrl Pts',(12.9722823229973,-0.0228334776507366,
4.47641814468844));
#31877=CARTESIAN_POINT('Ctrl Pts',(12.9958964391472,-0.24623199631158,4.40849164040747));
#31878=CARTESIAN_POINT('Ctrl Pts',(13.0195105552971,-0.410619302934066,
4.24266727085754));
#31879=CARTESIAN_POINT('Ctrl Pts',(13.0431246714469,-0.476598835156983,
4.01868600055616));
#31880=CARTESIAN_POINT('Ctrl Pts',(13.0667387875968,-0.428358138764893,
3.79022650014263));
#31881=CARTESIAN_POINT('Ctrl Pts',(13.0903529037467,-0.277458432473742,
3.61204067927388));
#31882=CARTESIAN_POINT('Ctrl Pts',(13.1139670198965,-0.060063881357403,
3.52683201033335));
#31883=CARTESIAN_POINT('Ctrl Pts',(13.1375811360464,0.171725397050831,3.55502134399878));
#31884=CARTESIAN_POINT('Ctrl Pts',(13.1611952521963,0.362359488617447,3.68985291022187));
#31885=CARTESIAN_POINT('Ctrl Pts',(13.1848093683461,0.466151606229838,3.89901338554908));
#31886=CARTESIAN_POINT('Ctrl Pts',(13.208423484496,0.458227246370285,4.13237600603144));
#31887=CARTESIAN_POINT('Ctrl Pts',(13.2320376006459,0.34048553704322,4.3340137951542));
#31888=CARTESIAN_POINT('Ctrl Pts',(13.2556517167957,0.141144098528766,4.45560285308526));
#31889=CARTESIAN_POINT('Ctrl Pts',(13.2792658329456,-0.0920235057499227,
4.46800351566886));
#31890=CARTESIAN_POINT('Ctrl Pts',(13.3028799490955,-0.30313703626889,4.36824387779166));
#31891=CARTESIAN_POINT('Ctrl Pts',(13.3264940652453,-0.441601665806575,
4.18023203113149));
#31892=CARTESIAN_POINT('Ctrl Pts',(13.3501081813952,-0.47423338199515,3.94902632355453));
#31893=CARTESIAN_POINT('Ctrl Pts',(13.3737222975451,-0.393211766889608,
3.73003681238273));
#31894=CARTESIAN_POINT('Ctrl Pts',(13.3973364136949,-0.217954214568861,
3.57574585842847));
#31895=CARTESIAN_POINT('Ctrl Pts',(13.4209505298448,0.00953758252632317,
3.52313036287841));
#31896=CARTESIAN_POINT('Ctrl Pts',(13.4445646459947,0.234743631574736,3.58479999551538));
#31897=CARTESIAN_POINT('Ctrl Pts',(13.4681787621445,0.403691735186444,3.74597519957476));
#31898=CARTESIAN_POINT('Ctrl Pts',(13.4917928782944,0.475892304226004,3.96802921540861));
#31899=CARTESIAN_POINT('Ctrl Pts',(13.5154069944443,0.434041969710506,4.19774525232923));
#31900=CARTESIAN_POINT('Ctrl Pts',(13.5390211105941,0.288170455640921,4.38007026295756));
#31901=CARTESIAN_POINT('Ctrl Pts',(13.562635226744,0.0732368858249759,4.47130878927046));
#31902=CARTESIAN_POINT('Ctrl Pts',(13.5862493428939,-0.159248413505658,
4.44959488329479));
#31903=CARTESIAN_POINT('Ctrl Pts',(13.6098634590437,-0.353568721957589,
4.32013243375547));
#31904=CARTESIAN_POINT('Ctrl Pts',(13.6334775751936,-0.46315382488092,4.1139480179165));
#31905=CARTESIAN_POINT('Ctrl Pts',(13.6570916913435,-0.461740889501104,
3.88045516635315));
#31906=CARTESIAN_POINT('Ctrl Pts',(13.6807058074933,-0.349668535617837,
3.67561206636528));
#31907=CARTESIAN_POINT('Ctrl Pts',(13.7043199236432,-0.153795683012805,
3.5485107928471));
#31908=CARTESIAN_POINT('Ctrl Pts',(13.7279340397931,0.0789353756500159,
3.5296120507922));
#31909=CARTESIAN_POINT('Ctrl Pts',(13.7515481559429,0.292749022042461,3.62344505529457));
#31910=CARTESIAN_POINT('Ctrl Pts',(13.7751622720928,0.436403327377467,3.80752207362193));
#31911=CARTESIAN_POINT('Ctrl Pts',(13.7987763882427,0.475470537355291,4.03772776690975));
#31912=CARTESIAN_POINT('Ctrl Pts',(13.8223905043925,0.400587923144683,4.25889173822189));
#31913=CARTESIAN_POINT('Ctrl Pts',(13.8460046205424,0.229701624524423,4.41801050223621));
#31914=CARTESIAN_POINT('Ctrl Pts',(13.8696187366923,0.00376573255618155,
4.47695013947711));
#31915=CARTESIAN_POINT('Ctrl Pts',(13.8932328528421,-0.223072643433687,
4.42158535558109));
#31916=CARTESIAN_POINT('Ctrl Pts',(13.916846968992,-0.396450107540549,4.26518470642179));
#31917=CARTESIAN_POINT('Ctrl Pts',(13.9404610851419,-0.474815543552022,
4.04523069632808));
#31918=CARTESIAN_POINT('Ctrl Pts',(13.9640752012917,-0.439388129199652,
3.81443683499316));
#31919=CARTESIAN_POINT('Ctrl Pts',(13.9876893174416,-0.298658290955197,
3.62811447792009));
#31920=CARTESIAN_POINT('Ctrl Pts',(14.0113034335915,-0.0863529142219465,
3.53091707503438));
#31921=CARTESIAN_POINT('Ctrl Pts',(14.0349175497413,0.146647539536438,3.54613866056158));
#31922=CARTESIAN_POINT('Ctrl Pts',(14.0585316658912,0.344502889581789,3.6701312755675));
#31923=CARTESIAN_POINT('Ctrl Pts',(14.0821457820411,0.459795723937725,3.87317922671144));
#31924=CARTESIAN_POINT('Ctrl Pts',(14.1057598981909,0.464895312258427,4.10662065901627));
#31925=CARTESIAN_POINT('Ctrl Pts',(14.1293740143408,0.358579502702881,4.31450970816539));
#31926=CARTESIAN_POINT('Ctrl Pts',(14.1529881304907,0.166327619131383,4.44702431634421));
#31927=CARTESIAN_POINT('Ctrl Pts',(14.1766022466405,-0.0657858362277661,
4.47240643522367));
#31928=CARTESIAN_POINT('Ctrl Pts',(14.2002163627904,-0.282133257977474,
4.38457306332079));
#31929=CARTESIAN_POINT('Ctrl Pts',(14.2238304789403,-0.430865480427841,
4.20457407964992));
#31930=CARTESIAN_POINT('Ctrl Pts',(14.2474445950901,-0.476337791093329,
3.97554749368157));
#31931=CARTESIAN_POINT('Ctrl Pts',(14.27105871124,-0.407652434174819,3.75238112107461));
#31932=CARTESIAN_POINT('Ctrl Pts',(14.2946728273899,-0.241270333599833,
3.58855833656088));
#31933=CARTESIAN_POINT('Ctrl Pts',(14.3182869435397,-0.0170661180132474,
3.52334041087493));
#31934=CARTESIAN_POINT('Ctrl Pts',(14.3419010596896,0.211228111558234,3.57235727391142));
#31935=CARTESIAN_POINT('Ctrl Pts',(14.3655151758395,0.388900053764453,3.72386169322071));
#31936=CARTESIAN_POINT('Ctrl Pts',(14.3891292919893,0.473369390821204,3.94154458004181));
#31937=CARTESIAN_POINT('Ctrl Pts',(14.4127434081392,0.444392458083208,4.17323671518384));
#31938=CARTESIAN_POINT('Ctrl Pts',(14.4363575242891,0.308913779199362,4.3634114655727));
#31939=CARTESIAN_POINT('Ctrl Pts',(14.4599716404389,0.0994017626770733,
4.46649212840691));
#31940=CARTESIAN_POINT('Ctrl Pts',(14.4835857565888,-0.133932578240045,
4.45777470525894));
#31941=CARTESIAN_POINT('Ctrl Pts',(14.5071998727387,-0.335169044432007,
4.33934838727104));
#31942=CARTESIAN_POINT('Ctrl Pts',(14.5308139888885,-0.456079915900645,
4.13959486595487));
#31943=CARTESIAN_POINT('Ctrl Pts',(14.5544281050384,-0.467688060597361,
3.90638646324521));
#31944=CARTESIAN_POINT('Ctrl Pts',(14.5780422211883,-0.367211505836647,
3.69561319629505));
#31945=CARTESIAN_POINT('Ctrl Pts',(14.6016563373381,-0.178730157419731,
3.55778834579073));
#31946=CARTESIAN_POINT('Ctrl Pts',(14.625270453488,0.0525851174261518,3.52594259660587));
#31947=CARTESIAN_POINT('Ctrl Pts',(14.6488845696379,0.271298002813252,3.60770800421126));
#31948=CARTESIAN_POINT('Ctrl Pts',(14.6724986857877,0.424992433239313,3.78348891949988));
#31949=CARTESIAN_POINT('Ctrl Pts',(14.6961128019376,0.476834468501385,4.01115822240469));
#31950=CARTESIAN_POINT('Ctrl Pts',(14.7197269180875,0.414399804028447,4.23615337970372));
#31951=CARTESIAN_POINT('Ctrl Pts',(14.7433410342373,0.252651341641402,4.40455273546398));
#31952=CARTESIAN_POINT('Ctrl Pts',(14.7669551503872,0.0303532266559796,
4.47599821226155));
#31953=CARTESIAN_POINT('Ctrl Pts',(14.7905692665371,-0.199219250862459,
4.43336740322118));
#31954=CARTESIAN_POINT('Ctrl Pts',(14.8141833826869,-0.381047447081096,
4.28687708064914));
#31955=CARTESIAN_POINT('Ctrl Pts',(14.8377974988368,-0.471554972144783,
4.07163466550741));
#31956=CARTESIAN_POINT('Ctrl Pts',(14.8614116149867,-0.449051060899263,
3.83922451083896));
#31957=CARTESIAN_POINT('Ctrl Pts',(14.8850257311365,-0.318928946727196,
3.64534530693059));
#31958=CARTESIAN_POINT('Ctrl Pts',(14.9086398472864,-0.112373269271187,
3.53646160000302));
#31959=CARTESIAN_POINT('Ctrl Pts',(14.9322539634362,0.121113399391719,3.5386680312482));
#31960=CARTESIAN_POINT('Ctrl Pts',(14.9558680795861,0.325574495333277,3.65143602219853));
#31961=CARTESIAN_POINT('Ctrl Pts',(14.979482195736,0.452009190454857,3.84773949289016));
#31962=CARTESIAN_POINT('Ctrl Pts',(15.0030963118858,0.470117180575255,4.08053390545391));
#31963=CARTESIAN_POINT('Ctrl Pts',(15.0267104280357,0.375557372208547,4.29402641177155));
#31964=CARTESIAN_POINT('Ctrl Pts',(15.0503245441856,0.190994688421392,4.43705643304037));
#31965=CARTESIAN_POINT('Ctrl Pts',(15.0739386603355,-0.0393454023191647,
4.47533644032795));
#31966=CARTESIAN_POINT('Ctrl Pts',(15.0975527764853,-0.260245916509526,
4.39971253597763));
#31967=CARTESIAN_POINT('Ctrl Pts',(15.1211668926352,-0.418792603204267,
4.22826540530875));
#31968=CARTESIAN_POINT('Ctrl Pts',(15.1369096367351,-0.457530945318996,
4.07754232577813));
#31969=CARTESIAN_POINT('Ctrl Pts',(15.1447810087851,-0.457870370902723,
4.00205890126089));
#31970=CARTESIAN_POINT('Ctrl Pts',(12.4850729970717,-0.208850989443975,
3.53079950502365));
#31971=CARTESIAN_POINT('Ctrl Pts',(12.4929443691216,-0.131499707516366,
3.49636882573344));
#31972=CARTESIAN_POINT('Ctrl Pts',(12.5086871132215,0.0404888716816997,
3.46654221242176));
#31973=CARTESIAN_POINT('Ctrl Pts',(12.5323012293714,0.288871199237585,3.54969213591223));
#31974=CARTESIAN_POINT('Ctrl Pts',(12.5559153455212,0.467986199318594,3.74075871022993));
#31975=CARTESIAN_POINT('Ctrl Pts',(12.5795294616711,0.534963825407437,3.99395832530641));
#31976=CARTESIAN_POINT('Ctrl Pts',(12.603143577821,0.473725169098917,4.24860452170932));
#31977=CARTESIAN_POINT('Ctrl Pts',(12.6267576939708,0.298958988020687,4.4436716456386));
#31978=CARTESIAN_POINT('Ctrl Pts',(12.6503718101207,0.0525433427838623,
4.53240944903922));
#31979=CARTESIAN_POINT('Ctrl Pts',(12.6739859262706,-0.206463809544117,
4.49355177571912));
#31980=CARTESIAN_POINT('Ctrl Pts',(12.6976000424205,-0.41599087873209,4.33641091237214));
#31981=CARTESIAN_POINT('Ctrl Pts',(12.7212141585703,-0.525822648369464,
4.09864686536754));
#31982=CARTESIAN_POINT('Ctrl Pts',(12.7448282747202,-0.509637448384189,
3.8372413948162));
#31983=CARTESIAN_POINT('Ctrl Pts',(12.76844239087,-0.37131404483003,3.61484216427635));
#31984=CARTESIAN_POINT('Ctrl Pts',(12.7920565070199,-0.144002664868576,
3.48474868689319));
#31985=CARTESIAN_POINT('Ctrl Pts',(12.8156706231698,0.117819965178516,3.47813877511649));
#31986=CARTESIAN_POINT('Ctrl Pts',(12.8392847393197,0.351406216185799,3.59659653799738));
#31987=CARTESIAN_POINT('Ctrl Pts',(12.8628988554695,0.500775523187073,3.81173274911973));
#31988=CARTESIAN_POINT('Ctrl Pts',(12.8865129716194,0.530130489073712,4.07198851734671));
#31989=CARTESIAN_POINT('Ctrl Pts',(12.9101270877692,0.432435993263294,4.31499173633021));
#31990=CARTESIAN_POINT('Ctrl Pts',(12.9337412039191,0.231105201134755,4.48250499290311));
#31991=CARTESIAN_POINT('Ctrl Pts',(12.957355320069,-0.0256115611541523,
4.53438256906268));
#31992=CARTESIAN_POINT('Ctrl Pts',(12.9809694362189,-0.276190334565159,
4.45819164252092));
#31993=CARTESIAN_POINT('Ctrl Pts',(13.0045835523687,-0.460578171623014,
4.27219189922559));
#31994=CARTESIAN_POINT('Ctrl Pts',(13.0281976685186,-0.534585243620437,
4.0209594724593));
#31995=CARTESIAN_POINT('Ctrl Pts',(13.0518117846684,-0.480475240551103,
3.76470396221295));
#31996=CARTESIAN_POINT('Ctrl Pts',(13.0754259008183,-0.311216001335094,
3.5648387853972));
#31997=CARTESIAN_POINT('Ctrl Pts',(13.0990400169682,-0.0673716809183137,
3.46926302296559));
#31998=CARTESIAN_POINT('Ctrl Pts',(13.122654133118,0.19261873182715,3.50088207171981));
#31999=CARTESIAN_POINT('Ctrl Pts',(13.1462682492679,0.406446724606302,3.65211820651514));
#32000=CARTESIAN_POINT('Ctrl Pts',(13.1698823654178,0.522866930420328,3.88672663484193));
#32001=CARTESIAN_POINT('Ctrl Pts',(13.1934964815676,0.513978436505609,4.14848181366307));
#32002=CARTESIAN_POINT('Ctrl Pts',(13.2171105977175,0.381911432304553,4.37465229220773));
#32003=CARTESIAN_POINT('Ctrl Pts',(13.2407247138674,0.158316694737061,4.51103474084347));
#32004=CARTESIAN_POINT('Ctrl Pts',(13.2643388300172,-0.103219740820234,
4.52494415635039));
#32005=CARTESIAN_POINT('Ctrl Pts',(13.2879529461671,-0.340018846942428,
4.41304705047411));
#32006=CARTESIAN_POINT('Ctrl Pts',(13.311567062317,-0.495330069408668,4.20216034359148));
#32007=CARTESIAN_POINT('Ctrl Pts',(13.3351811784669,-0.531931992580964,
3.94282450306062));
#32008=CARTESIAN_POINT('Ctrl Pts',(13.3587952946167,-0.44105271077271,3.69719116838925));
#32009=CARTESIAN_POINT('Ctrl Pts',(13.3824094107666,-0.244472076510672,
3.5241280781681));
#32010=CARTESIAN_POINT('Ctrl Pts',(13.4060235269164,0.0106979927399635,
3.46511100671938));
#32011=CARTESIAN_POINT('Ctrl Pts',(13.4296376430663,0.263304213558122,3.53428380605355));
#32012=CARTESIAN_POINT('Ctrl Pts',(13.4532517592162,0.452807746647384,3.71506873327496));
#32013=CARTESIAN_POINT('Ctrl Pts',(13.476865875366,0.533792751104717,3.96413942206993));
#32014=CARTESIAN_POINT('Ctrl Pts',(13.5004799915159,0.486850606847911,4.22180434800346));
#32015=CARTESIAN_POINT('Ctrl Pts',(13.5240941076658,0.323231325528255,4.42631231788287));
#32016=CARTESIAN_POINT('Ctrl Pts',(13.5477082238157,0.0821474069231642,
4.52865157307741));
#32017=CARTESIAN_POINT('Ctrl Pts',(13.5713223399655,-0.178623709606947,
4.50429579866153));
#32018=CARTESIAN_POINT('Ctrl Pts',(13.5949364561154,-0.396586410669692,
4.35908202552279));
#32019=CARTESIAN_POINT('Ctrl Pts',(13.6185505722652,-0.519504417643299,
4.12781174527607));
#32020=CARTESIAN_POINT('Ctrl Pts',(13.6421646884151,-0.517919574482721,
3.86591049053316));
#32021=CARTESIAN_POINT('Ctrl Pts',(13.665778804565,-0.392211699884016,3.6361447201764));
#32022=CARTESIAN_POINT('Ctrl Pts',(13.6893929207148,-0.172507561089802,
3.49357940054904));
#32023=CARTESIAN_POINT('Ctrl Pts',(13.7130070368647,0.0885392156030666,
3.47238130294519));
#32024=CARTESIAN_POINT('Ctrl Pts',(13.7366211530146,0.328366952925232,3.57763069902274));
#32025=CARTESIAN_POINT('Ctrl Pts',(13.7602352691644,0.489499264105438,3.78410383833506));
#32026=CARTESIAN_POINT('Ctrl Pts',(13.7838493853143,0.533319669072828,4.04231799571659));
#32027=CARTESIAN_POINT('Ctrl Pts',(13.8074635014642,0.449326302728307,4.29039035083475));
#32028=CARTESIAN_POINT('Ctrl Pts',(13.831077617614,0.257648760022572,4.46886863686992));
#32029=CARTESIAN_POINT('Ctrl Pts',(13.8546917337639,0.00422389839726028,
4.53497929012603));
#32030=CARTESIAN_POINT('Ctrl Pts',(13.8783058499138,-0.25021324988294,4.47287843233165));
#32031=CARTESIAN_POINT('Ctrl Pts',(13.9019199660636,-0.444685051009628,
4.29744896636227));
#32032=CARTESIAN_POINT('Ctrl Pts',(13.9255340822135,-0.532584984058807,
4.05073378496132));
#32033=CARTESIAN_POINT('Ctrl Pts',(13.9491481983634,-0.492847218174075,
3.79185989881933));
#32034=CARTESIAN_POINT('Ctrl Pts',(13.9727623145132,-0.334995185577738,
3.58286823685896));
#32035=CARTESIAN_POINT('Ctrl Pts',(13.9963764306631,-0.0968592247428986,
3.47384510573062));
#32036=CARTESIAN_POINT('Ctrl Pts',(14.019990546813,0.164489723571401,3.49091865775613));
#32037=CARTESIAN_POINT('Ctrl Pts',(14.0436046629628,0.386417564563212,3.62999709733779));
#32038=CARTESIAN_POINT('Ctrl Pts',(14.0672187791127,0.515737746224078,3.85774930825782));
#32039=CARTESIAN_POINT('Ctrl Pts',(14.0908328952626,0.521457786777448,4.11959288770904));
#32040=CARTESIAN_POINT('Ctrl Pts',(14.1144470114124,0.402206838685568,4.35277519909424));
#32041=CARTESIAN_POINT('Ctrl Pts',(14.1380611275623,0.186564221804844,4.50141247822903));
#32042=CARTESIAN_POINT('Ctrl Pts',(14.1616752437122,-0.0737898095680628,
4.52988276645436));
#32043=CARTESIAN_POINT('Ctrl Pts',(14.185289359862,-0.316459599402161,4.43136296100575));
#32044=CARTESIAN_POINT('Ctrl Pts',(14.2089034760119,-0.483287643257218,
4.22946401908862));
#32045=CARTESIAN_POINT('Ctrl Pts',(14.2325175921618,-0.53429243907693,3.97257242762026));
#32046=CARTESIAN_POINT('Ctrl Pts',(14.2561317083116,-0.457250332481466,
3.72225404480531));
#32047=CARTESIAN_POINT('Ctrl Pts',(14.2797458244615,-0.270625000632592,
3.53849941363631));
#32048=CARTESIAN_POINT('Ctrl Pts',(14.3033599406114,-0.0191425034699505,
3.46534661065105));
#32049=CARTESIAN_POINT('Ctrl Pts',(14.3269740567612,0.236927627906706,3.52032721432634));
#32050=CARTESIAN_POINT('Ctrl Pts',(14.3505881729111,0.436216403922163,3.69026474025285));
#32051=CARTESIAN_POINT('Ctrl Pts',(14.374202289061,0.530962882087739,3.93443247734966));
#32052=CARTESIAN_POINT('Ctrl Pts',(14.3978164052108,0.498460409348769,4.19431392768733));
#32053=CARTESIAN_POINT('Ctrl Pts',(14.4214305213607,0.346498429557861,4.40762669256976));
#32054=CARTESIAN_POINT('Ctrl Pts',(14.4450446375106,0.111495689030631,4.52324888295055));
#32055=CARTESIAN_POINT('Ctrl Pts',(14.4686587536604,-0.150227769531968,
4.51347083601981));
#32056=CARTESIAN_POINT('Ctrl Pts',(14.4922728698103,-0.375948097339969,
4.38063592879268));
#32057=CARTESIAN_POINT('Ctrl Pts',(14.5158869859602,-0.51156984651846,4.15657897149511));
#32058=CARTESIAN_POINT('Ctrl Pts',(14.53950110211,-0.52459032076832,3.89499677367918));
#32059=CARTESIAN_POINT('Ctrl Pts',(14.5631152182599,-0.411889072794842,
3.65857933001481));
#32060=CARTESIAN_POINT('Ctrl Pts',(14.5867293344098,-0.200475741228102,
3.50398572665543));
#32061=CARTESIAN_POINT('Ctrl Pts',(14.6103434505596,0.0589829973059192,
3.46826539682992));
#32062=CARTESIAN_POINT('Ctrl Pts',(14.6339575667095,0.304306049929579,3.5599789662306));
#32063=CARTESIAN_POINT('Ctrl Pts',(14.6575716828594,0.476700039321847,3.75714663952638));
#32064=CARTESIAN_POINT('Ctrl Pts',(14.6811857990092,0.53484954579562,4.0125158112076));
#32065=CARTESIAN_POINT('Ctrl Pts',(14.7047999151591,0.464818635404008,4.26488548168423));
#32066=CARTESIAN_POINT('Ctrl Pts',(14.728414031309,0.283390703164248,4.45377350235044));
#32067=CARTESIAN_POINT('Ctrl Pts',(14.7520281474588,0.0340462163765225,
4.5339115446661));
#32068=CARTESIAN_POINT('Ctrl Pts',(14.7756422636087,-0.223457683695575,
4.48609396779546));
#32069=CARTESIAN_POINT('Ctrl Pts',(14.7992563797586,-0.427408393186059,
4.32178058932398));
#32070=CARTESIAN_POINT('Ctrl Pts',(14.8228704959084,-0.528927708313459,
4.08035024907128));
#32071=CARTESIAN_POINT('Ctrl Pts',(14.8464846120583,-0.503685810960444,
3.81966341983811));
#32072=CARTESIAN_POINT('Ctrl Pts',(14.8700987282082,-0.357732113691821,
3.6021954912391));
#32073=CARTESIAN_POINT('Ctrl Pts',(14.893712844358,-0.126045401495737,3.48006421709321));
#32074=CARTESIAN_POINT('Ctrl Pts',(14.9173269605079,0.13584891809103,3.48253909847714));
#32075=CARTESIAN_POINT('Ctrl Pts',(14.9409410766578,0.365186207068703,3.60902724630258));
#32076=CARTESIAN_POINT('Ctrl Pts',(14.9645551928076,0.507003847624586,3.82921439524653));
#32077=CARTESIAN_POINT('Ctrl Pts',(14.9881693089575,0.52731498478211,4.0903322339271));
#32078=CARTESIAN_POINT('Ctrl Pts',(15.0117834251074,0.421250356706029,4.32979975898591));
#32079=CARTESIAN_POINT('Ctrl Pts',(15.0353975412572,0.214232462415332,4.49023183125449));
#32080=CARTESIAN_POINT('Ctrl Pts',(15.0590116574071,-0.0441324441701724,
4.53316925684615));
#32081=CARTESIAN_POINT('Ctrl Pts',(15.082625773557,-0.291909288096862,4.4483444097243));
#32082=CARTESIAN_POINT('Ctrl Pts',(15.1062398897068,-0.469745893811612,
4.25603780014884));
#32083=CARTESIAN_POINT('Ctrl Pts',(15.1219826338067,-0.513197418509596,
4.08697667736293));
#32084=CARTESIAN_POINT('Ctrl Pts',(15.1298540058567,-0.513578141027115,
4.0023094018511));
#32085=CARTESIAN_POINT('Ctrl Pts',(12.4701459941433,-0.231505035597357,
3.47990537377399));
#32086=CARTESIAN_POINT('Ctrl Pts',(12.4780173661933,-0.145763467775118,
3.44174000210903));
#32087=CARTESIAN_POINT('Ctrl Pts',(12.4937601102932,0.0448806955855158,
3.40867809900361));
#32088=CARTESIAN_POINT('Ctrl Pts',(12.517374226443,0.320205029627059,3.5008472864651));
#32089=CARTESIAN_POINT('Ctrl Pts',(12.5409883425929,0.518748616038451,3.71263883318769));
#32090=CARTESIAN_POINT('Ctrl Pts',(12.5646024587428,0.592991298599855,3.99330298545039));
#32091=CARTESIAN_POINT('Ctrl Pts',(12.5882165748926,0.525110091302815,4.27557062957281));
#32092=CARTESIAN_POINT('Ctrl Pts',(12.6118306910425,0.331387039860997,4.49179666512739));
#32093=CARTESIAN_POINT('Ctrl Pts',(12.6354448071924,0.0582427139750047,
4.5901598492798));
#32094=CARTESIAN_POINT('Ctrl Pts',(12.6590589233422,-0.22885891853004,4.54708728798072));
#32095=CARTESIAN_POINT('Ctrl Pts',(12.6826730394921,-0.461113368174311,
4.37290137073994));
#32096=CARTESIAN_POINT('Ctrl Pts',(12.706287155642,-0.582858578993347,4.10934708109011));
#32097=CARTESIAN_POINT('Ctrl Pts',(12.7299012717918,-0.564917771967644,
3.8195869850214));
#32098=CARTESIAN_POINT('Ctrl Pts',(12.7535153879417,-0.411590442520908,
3.57306413195747));
#32099=CARTESIAN_POINT('Ctrl Pts',(12.7771295040916,-0.159622619673808,
3.42885942795892));
#32100=CARTESIAN_POINT('Ctrl Pts',(12.8007436202414,0.130599885139872,3.42153253970604));
#32101=CARTESIAN_POINT('Ctrl Pts',(12.8243577363913,0.38952321367407,3.55283940440193));
#32102=CARTESIAN_POINT('Ctrl Pts',(12.8479718525412,0.555094594621529,3.79131141905102));
#32103=CARTESIAN_POINT('Ctrl Pts',(12.871585968691,0.587633690752404,4.07979710469805));
#32104=CARTESIAN_POINT('Ctrl Pts',(12.8952000848409,0.479342282651013,4.34915885879276));
#32105=CARTESIAN_POINT('Ctrl Pts',(12.9188142009908,0.256173159427565,4.53484226172604));
#32106=CARTESIAN_POINT('Ctrl Pts',(12.9424283171406,-0.0283896446575681,
4.59234699343691));
#32107=CARTESIAN_POINT('Ctrl Pts',(12.9660424332905,-0.306148672818738,
4.50789164463438));
#32108=CARTESIAN_POINT('Ctrl Pts',(12.9896565494404,-0.510537040311962,
4.30171652759364));
#32109=CARTESIAN_POINT('Ctrl Pts',(13.0132706655902,-0.59257165208389,4.02323294436244));
#32110=CARTESIAN_POINT('Ctrl Pts',(13.0368847817401,-0.532592342337314,
3.73918142428326));
#32111=CARTESIAN_POINT('Ctrl Pts',(13.06049889789,-0.344973570196446,3.51763689152052));
#32112=CARTESIAN_POINT('Ctrl Pts',(13.0841130140398,-0.0746794804792245,
3.41169403559782));
#32113=CARTESIAN_POINT('Ctrl Pts',(13.1077271301897,0.213512066603468,3.44674279944083));
#32114=CARTESIAN_POINT('Ctrl Pts',(13.1313412463396,0.450533960595157,3.6143835028084));
#32115=CARTESIAN_POINT('Ctrl Pts',(13.1549553624894,0.579582254610818,3.87443988413478));
#32116=CARTESIAN_POINT('Ctrl Pts',(13.1785694786393,0.569729626640933,4.1645876212947));
#32117=CARTESIAN_POINT('Ctrl Pts',(13.2021835947892,0.423337327565886,4.41529078926125));
#32118=CARTESIAN_POINT('Ctrl Pts',(13.225797710939,0.175489290945357,4.56646662860168));
#32119=CARTESIAN_POINT('Ctrl Pts',(13.2494118270889,-0.114415975890545,
4.58188479703192));
#32120=CARTESIAN_POINT('Ctrl Pts',(13.2730259432388,-0.376900657615966,
4.45785022315656));
#32121=CARTESIAN_POINT('Ctrl Pts',(13.2966400593886,-0.54905847301076,4.22408865605146));
#32122=CARTESIAN_POINT('Ctrl Pts',(13.3202541755385,-0.589630603166779,
3.93662268256671));
#32123=CARTESIAN_POINT('Ctrl Pts',(13.3438682916884,-0.488893654655812,
3.66434552439578));
#32124=CARTESIAN_POINT('Ctrl Pts',(13.3674824078382,-0.270989938452484,
3.47251029790774));
#32125=CARTESIAN_POINT('Ctrl Pts',(13.3910965239881,0.0118584029536041,
3.40709165056035));
#32126=CARTESIAN_POINT('Ctrl Pts',(13.414710640138,0.291864795541507,3.48376761659174));
#32127=CARTESIAN_POINT('Ctrl Pts',(13.4383247562878,0.501923758108325,3.68416226697515));
#32128=CARTESIAN_POINT('Ctrl Pts',(13.4619388724377,0.591693197983429,3.96024962873126));
#32129=CARTESIAN_POINT('Ctrl Pts',(13.4855529885876,0.539659243985316,4.2458634436777));
#32130=CARTESIAN_POINT('Ctrl Pts',(13.5091671047374,0.358292195415589,4.47255437280819));
#32131=CARTESIAN_POINT('Ctrl Pts',(13.5327812208873,0.0910579280213527,
4.58599435688436));
#32132=CARTESIAN_POINT('Ctrl Pts',(13.5563953370372,-0.197999005708236,
4.55899671402827));
#32133=CARTESIAN_POINT('Ctrl Pts',(13.580009453187,-0.439604099381795,4.39803161729011));
#32134=CARTESIAN_POINT('Ctrl Pts',(13.6036235693369,-0.575855010405679,
4.14167547263565));
#32135=CARTESIAN_POINT('Ctrl Pts',(13.6272376854868,-0.574098259464336,
3.85136581471317));
#32136=CARTESIAN_POINT('Ctrl Pts',(13.6508518016366,-0.434754864150196,
3.59667737398752));
#32137=CARTESIAN_POINT('Ctrl Pts',(13.6744659177865,-0.191219439166798,
3.43864800825098));
#32138=CARTESIAN_POINT('Ctrl Pts',(13.6980800339364,0.0981430555561168,
3.41515055509818));
#32139=CARTESIAN_POINT('Ctrl Pts',(13.7216941500862,0.363984883808003,3.53181634275091));
#32140=CARTESIAN_POINT('Ctrl Pts',(13.7453082662361,0.54259520083341,3.76068560304818));
#32141=CARTESIAN_POINT('Ctrl Pts',(13.768922382386,0.591168800790367,4.04690822452342));
#32142=CARTESIAN_POINT('Ctrl Pts',(13.7925364985358,0.498064682311931,4.32188896344761));
#32143=CARTESIAN_POINT('Ctrl Pts',(13.8161506146857,0.28559589552072,4.51972677150362));
#32144=CARTESIAN_POINT('Ctrl Pts',(13.8397647308356,0.00468206423833927,
4.59300844077494));
#32145=CARTESIAN_POINT('Ctrl Pts',(13.8633788469854,-0.277353856332193,
4.52417150908221));
#32146=CARTESIAN_POINT('Ctrl Pts',(13.8869929631353,-0.492919994478707,
4.32971322630275));
#32147=CARTESIAN_POINT('Ctrl Pts',(13.9106070792852,-0.590354424565592,
4.05623687359455));
#32148=CARTESIAN_POINT('Ctrl Pts',(13.934221195435,-0.546306307148498,3.76928296264551));
#32149=CARTESIAN_POINT('Ctrl Pts',(13.9578353115849,-0.371332080200278,
3.53762199579782));
#32150=CARTESIAN_POINT('Ctrl Pts',(13.9814494277348,-0.107365535263851,
3.41677313642685));
#32151=CARTESIAN_POINT('Ctrl Pts',(14.0050635438846,0.182331907606365,3.43569865495067));
#32152=CARTESIAN_POINT('Ctrl Pts',(14.0286776600345,0.428332239544634,3.58986291910809));
#32153=CARTESIAN_POINT('Ctrl Pts',(14.0522917761844,0.571679768510432,3.8423193898042));
#32154=CARTESIAN_POINT('Ctrl Pts',(14.0759058923342,0.578020261296468,4.1325651164018));
#32155=CARTESIAN_POINT('Ctrl Pts',(14.0995200084841,0.445834174668256,4.39104069002309));
#32156=CARTESIAN_POINT('Ctrl Pts',(14.123134124634,0.206800824478305,4.55580064011384));
#32157=CARTESIAN_POINT('Ctrl Pts',(14.1467482407838,-0.0817937829083601,
4.58735909768505));
#32158=CARTESIAN_POINT('Ctrl Pts',(14.1703623569337,-0.350785940826847,
4.4781528586907));
#32159=CARTESIAN_POINT('Ctrl Pts',(14.1939764730836,-0.535709806086595,
4.25435395852733));
#32160=CARTESIAN_POINT('Ctrl Pts',(14.2175905892334,-0.59224708706053,3.96959736155895));
#32161=CARTESIAN_POINT('Ctrl Pts',(14.2412047053833,-0.506848230788112,
3.69212696853602));
#32162=CARTESIAN_POINT('Ctrl Pts',(14.2648188215332,-0.29997966766535,3.48844049071174));
#32163=CARTESIAN_POINT('Ctrl Pts',(14.288432937683,-0.0212188889266537,
3.40735281042717));
#32164=CARTESIAN_POINT('Ctrl Pts',(14.3120470538329,0.262627144255178,3.46829715474127));
#32165=CARTESIAN_POINT('Ctrl Pts',(14.3356611699828,0.483532754079872,3.65666778728498));
#32166=CARTESIAN_POINT('Ctrl Pts',(14.3592752861326,0.588556373354274,3.9273203746575));
#32167=CARTESIAN_POINT('Ctrl Pts',(14.3828894022825,0.55252836061433,4.21539114019081));
#32168=CARTESIAN_POINT('Ctrl Pts',(14.4065035184324,0.384083079916361,4.45184191956682));
#32169=CARTESIAN_POINT('Ctrl Pts',(14.4301176345822,0.123589615384189,4.58000563749418));
#32170=CARTESIAN_POINT('Ctrl Pts',(14.4537317507321,-0.166522960823891,
4.56916696678068));
#32171=CARTESIAN_POINT('Ctrl Pts',(14.477345866882,-0.416727150247931,4.42192347031433));
#32172=CARTESIAN_POINT('Ctrl Pts',(14.5009599830318,-0.567059777136274,
4.17356307703535));
#32173=CARTESIAN_POINT('Ctrl Pts',(14.5245740991817,-0.58149258093928,3.88360708411314));
#32174=CARTESIAN_POINT('Ctrl Pts',(14.5481882153316,-0.456566639753037,
3.62154546373458));
#32175=CARTESIAN_POINT('Ctrl Pts',(14.5718023314814,-0.222221325036472,
3.45018310752014));
#32176=CARTESIAN_POINT('Ctrl Pts',(14.5954164476313,0.0653808771856868,
3.41058819705396));
#32177=CARTESIAN_POINT('Ctrl Pts',(14.6190305637812,0.337314097045906,3.51224992824993));
#32178=CARTESIAN_POINT('Ctrl Pts',(14.642644679931,0.528407645404381,3.73080435955289));
#32179=CARTESIAN_POINT('Ctrl Pts',(14.6662587960809,0.592864623089856,4.0138734000105));
#32180=CARTESIAN_POINT('Ctrl Pts',(14.6898729122308,0.515237466779568,4.29361758366474));
#32181=CARTESIAN_POINT('Ctrl Pts',(14.7134870283806,0.314130064687094,4.5029942692369));
#32182=CARTESIAN_POINT('Ctrl Pts',(14.7371011445305,0.0377392060970651,
4.59182487707066));
#32183=CARTESIAN_POINT('Ctrl Pts',(14.7607152606804,-0.24769611652869,4.53882053236973));
#32184=CARTESIAN_POINT('Ctrl Pts',(14.7843293768302,-0.47376933929102,4.35668409799883));
#32185=CARTESIAN_POINT('Ctrl Pts',(14.8079434929801,-0.586300444482135,
4.08906583263515));
#32186=CARTESIAN_POINT('Ctrl Pts',(14.83155760913,-0.558320561021625,3.80010232883727));
#32187=CARTESIAN_POINT('Ctrl Pts',(14.8551717252798,-0.396535280656446,
3.55904567554761));
#32188=CARTESIAN_POINT('Ctrl Pts',(14.8787858414297,-0.139717533720287,
3.42366683418339));
#32189=CARTESIAN_POINT('Ctrl Pts',(14.9023999575795,0.150584436790342,3.42641016570609));
#32190=CARTESIAN_POINT('Ctrl Pts',(14.9260140737294,0.404797918804129,3.56661847040663));
#32191=CARTESIAN_POINT('Ctrl Pts',(14.9496281898793,0.561998504794314,3.8106892976029));
#32192=CARTESIAN_POINT('Ctrl Pts',(14.9732423060292,0.584512788988964,4.10013056240029));
#32193=CARTESIAN_POINT('Ctrl Pts',(14.996856422179,0.466943341203511,4.36557310620026));
#32194=CARTESIAN_POINT('Ctrl Pts',(15.0204705383289,0.237470236409271,4.54340722946861));
#32195=CARTESIAN_POINT('Ctrl Pts',(15.0440846544788,-0.0489194860211801,
4.59100207336435));
#32196=CARTESIAN_POINT('Ctrl Pts',(15.0676987706286,-0.323572659684198,
4.49697628347096));
#32197=CARTESIAN_POINT('Ctrl Pts',(15.0913128867785,-0.520699184418956,
4.28381019498893));
#32198=CARTESIAN_POINT('Ctrl Pts',(15.1070556308784,-0.568863891700195,
4.09641102894772));
#32199=CARTESIAN_POINT('Ctrl Pts',(15.1149270029284,-0.569285911151507,
4.00255990244131));
#32200=CARTESIAN_POINT('Ctrl Pts',(12.455218991215,-0.25415908175074,3.42901124252432));
#32201=CARTESIAN_POINT('Ctrl Pts',(12.4630903632649,-0.16002722803387,3.38711117848463));
#32202=CARTESIAN_POINT('Ctrl Pts',(12.4788331073648,0.0492725194893315,
3.35081398558546));
#32203=CARTESIAN_POINT('Ctrl Pts',(12.5024472235147,0.351538860016532,3.45200243701797));
#32204=CARTESIAN_POINT('Ctrl Pts',(12.5260613396645,0.569511032758309,3.68451895614546));
#32205=CARTESIAN_POINT('Ctrl Pts',(12.5496754558144,0.651018771792273,3.99264764559437));
#32206=CARTESIAN_POINT('Ctrl Pts',(12.5732895719643,0.576495013506714,4.3025367374363));
#32207=CARTESIAN_POINT('Ctrl Pts',(12.5969036881141,0.363815091701307,4.53992168461618));
#32208=CARTESIAN_POINT('Ctrl Pts',(12.620517804264,0.0639420851661475,4.64791024952038));
#32209=CARTESIAN_POINT('Ctrl Pts',(12.6441319204139,-0.251254027515963,
4.60062280024232));
#32210=CARTESIAN_POINT('Ctrl Pts',(12.6677460365637,-0.506235857616531,
4.40939182910775));
#32211=CARTESIAN_POINT('Ctrl Pts',(12.6913601527136,-0.639894509617229,
4.12004729681268));
#32212=CARTESIAN_POINT('Ctrl Pts',(12.7149742688635,-0.620198095551099,
3.8019325752266));
#32213=CARTESIAN_POINT('Ctrl Pts',(12.7385883850133,-0.451866840211785,
3.53128609963859));
#32214=CARTESIAN_POINT('Ctrl Pts',(12.7622025011632,-0.17524257447904,3.37297016902465));
#32215=CARTESIAN_POINT('Ctrl Pts',(12.7858166173131,0.143379805101228,3.36492630429559));
#32216=CARTESIAN_POINT('Ctrl Pts',(12.809430733463,0.42764021116234,3.50908227080648));
#32217=CARTESIAN_POINT('Ctrl Pts',(12.8330448496128,0.609413666055986,3.77089008898231));
#32218=CARTESIAN_POINT('Ctrl Pts',(12.8566589657627,0.645136892431096,4.08760569204938));
#32219=CARTESIAN_POINT('Ctrl Pts',(12.8802730819125,0.526248572038732,4.38332598125533));
#32220=CARTESIAN_POINT('Ctrl Pts',(12.9038871980624,0.281241117720374,4.58717953054897));
#32221=CARTESIAN_POINT('Ctrl Pts',(12.9275013142123,-0.0311677281609838,
4.65031141781114));
#32222=CARTESIAN_POINT('Ctrl Pts',(12.9511154303622,-0.336107011072318,
4.55759164674784));
#32223=CARTESIAN_POINT('Ctrl Pts',(12.974729546512,-0.56049590900091,4.33124115596169));
#32224=CARTESIAN_POINT('Ctrl Pts',(12.9983436626619,-0.650558060547343,
4.02550641626558));
#32225=CARTESIAN_POINT('Ctrl Pts',(13.0219577788117,-0.584709444123524,
3.71365888635357));
#32226=CARTESIAN_POINT('Ctrl Pts',(13.0455718949616,-0.378731139057797,
3.47043499764384));
#32227=CARTESIAN_POINT('Ctrl Pts',(13.0691860111115,-0.0819872800401352,
3.35412504823007));
#32228=CARTESIAN_POINT('Ctrl Pts',(13.0928001272613,0.234405401379786,3.39260352716186));
#32229=CARTESIAN_POINT('Ctrl Pts',(13.1164142434112,0.494621196584012,3.57664879910166));
#32230=CARTESIAN_POINT('Ctrl Pts',(13.1400283595611,0.636297578801308,3.86215313342763));
#32231=CARTESIAN_POINT('Ctrl Pts',(13.1636424757109,0.625480816776257,4.18069342892634));
#32232=CARTESIAN_POINT('Ctrl Pts',(13.1872565918608,0.464763222827219,4.45592928631477));
#32233=CARTESIAN_POINT('Ctrl Pts',(13.2108707080107,0.192661887153653,4.62189851635989));
#32234=CARTESIAN_POINT('Ctrl Pts',(13.2344848241605,-0.125612210960856,
4.63882543771344));
#32235=CARTESIAN_POINT('Ctrl Pts',(13.2580989403104,-0.413782468289504,
4.50265339583901));
#32236=CARTESIAN_POINT('Ctrl Pts',(13.2817130564603,-0.602786876612853,
4.24601696851145));
#32237=CARTESIAN_POINT('Ctrl Pts',(13.3053271726101,-0.647329213752593,
3.9304208620728));
#32238=CARTESIAN_POINT('Ctrl Pts',(13.32894128876,-0.536734598538914,3.6314998804023));
#32239=CARTESIAN_POINT('Ctrl Pts',(13.3525554049099,-0.297507800394296,
3.42089251764738));
#32240=CARTESIAN_POINT('Ctrl Pts',(13.3761695210598,0.0130188131672444,
3.34907229440132));
#32241=CARTESIAN_POINT('Ctrl Pts',(13.3997836372096,0.320425377524893,3.43325142712992));
#32242=CARTESIAN_POINT('Ctrl Pts',(13.4233977533595,0.551039769569266,3.65325580067535));
#32243=CARTESIAN_POINT('Ctrl Pts',(13.4470118695093,0.649593644862141,3.95635983539258));
#32244=CARTESIAN_POINT('Ctrl Pts',(13.4706259856592,0.592467881122722,4.26992253935193));
#32245=CARTESIAN_POINT('Ctrl Pts',(13.4942401018091,0.393353065302923,4.5187964277335));
#32246=CARTESIAN_POINT('Ctrl Pts',(13.5178542179589,0.0999684491195412,
4.64333714069132));
#32247=CARTESIAN_POINT('Ctrl Pts',(13.5414683341088,-0.217374301809525,
4.61369762939502));
#32248=CARTESIAN_POINT('Ctrl Pts',(13.5650824502587,-0.482621788093898,
4.43698120905743));
#32249=CARTESIAN_POINT('Ctrl Pts',(13.5886965664085,-0.632205603168059,
4.15553919999523));
#32250=CARTESIAN_POINT('Ctrl Pts',(13.6123106825584,-0.630276944445953,
3.83682113889318));
#32251=CARTESIAN_POINT('Ctrl Pts',(13.6359247987083,-0.477298028416376,
3.55721002779864));
#32252=CARTESIAN_POINT('Ctrl Pts',(13.6595389148582,-0.209931317243796,
3.38371661595291));
#32253=CARTESIAN_POINT('Ctrl Pts',(13.683153031008,0.107746895509167,3.35791980725116));
#32254=CARTESIAN_POINT('Ctrl Pts',(13.7067671471579,0.399602814690774,3.48600198647908));
#32255=CARTESIAN_POINT('Ctrl Pts',(13.7303812633077,0.59569113756138,3.73726736776131));
#32256=CARTESIAN_POINT('Ctrl Pts',(13.7539953794576,0.649017932507905,4.05149845333026));
#32257=CARTESIAN_POINT('Ctrl Pts',(13.7776094956075,0.546803061895555,4.35338757606046));
#32258=CARTESIAN_POINT('Ctrl Pts',(13.8012236117573,0.313543031018869,4.57058490613733));
#32259=CARTESIAN_POINT('Ctrl Pts',(13.8248377279072,0.00514023007941788,
4.65103759142385));
#32260=CARTESIAN_POINT('Ctrl Pts',(13.8484518440571,-0.304494462781446,
4.57546458583277));
#32261=CARTESIAN_POINT('Ctrl Pts',(13.8720659602069,-0.541154937947787,
4.36197748624323));
#32262=CARTESIAN_POINT('Ctrl Pts',(13.8956800763568,-0.648123865072376,
4.06173996222779));
#32263=CARTESIAN_POINT('Ctrl Pts',(13.9192941925067,-0.599765396122921,
3.74670602647169));
#32264=CARTESIAN_POINT('Ctrl Pts',(13.9429083086565,-0.407668974822819,
3.49237575473668));
#32265=CARTESIAN_POINT('Ctrl Pts',(13.9665224248064,-0.117871845784803,
3.35970116712309));
#32266=CARTESIAN_POINT('Ctrl Pts',(13.9901365409563,0.200174091641329,3.38047865214521));
#32267=CARTESIAN_POINT('Ctrl Pts',(14.0137506571061,0.470246914526057,3.54972874087838));
#32268=CARTESIAN_POINT('Ctrl Pts',(14.037364773256,0.627621790796785,3.82688947135059));
#32269=CARTESIAN_POINT('Ctrl Pts',(14.0609788894059,0.634582735815489,4.14553734509456));
#32270=CARTESIAN_POINT('Ctrl Pts',(14.0845930055557,0.489461510650943,4.42930618095194));
#32271=CARTESIAN_POINT('Ctrl Pts',(14.1082071217056,0.227037427151766,4.61018880199865));
#32272=CARTESIAN_POINT('Ctrl Pts',(14.1318212378555,-0.0897977562486571,
4.64483542891575));
#32273=CARTESIAN_POINT('Ctrl Pts',(14.1554353540053,-0.385112282251534,
4.52494275637564));
#32274=CARTESIAN_POINT('Ctrl Pts',(14.1790494701552,-0.588131968915973,
4.27924389796604));
#32275=CARTESIAN_POINT('Ctrl Pts',(14.2026635863051,-0.65020173504413,3.96662229549764));
#32276=CARTESIAN_POINT('Ctrl Pts',(14.2262777024549,-0.556446129094758,
3.66199989226673));
#32277=CARTESIAN_POINT('Ctrl Pts',(14.2498918186048,-0.329334334698108,
3.43838156778717));
#32278=CARTESIAN_POINT('Ctrl Pts',(14.2735059347547,-0.0232952743833569,
3.34935901020328));
#32279=CARTESIAN_POINT('Ctrl Pts',(14.2971200509045,0.28832666060365,3.41626709515619));
#32280=CARTESIAN_POINT('Ctrl Pts',(14.3207341670544,0.530849104237583,3.62307083431711));
#32281=CARTESIAN_POINT('Ctrl Pts',(14.3443482832043,0.646149864620809,3.92020827196535));
#32282=CARTESIAN_POINT('Ctrl Pts',(14.3679623993541,0.606596311879891,4.2364683526943));
#32283=CARTESIAN_POINT('Ctrl Pts',(14.391576515504,0.42166773027486,4.49605714656388));
#32284=CARTESIAN_POINT('Ctrl Pts',(14.4151906316539,0.135683541737747,4.63676239203782));
#32285=CARTESIAN_POINT('Ctrl Pts',(14.4388047478037,-0.182818152115814,
4.62486309754155));
#32286=CARTESIAN_POINT('Ctrl Pts',(14.4624188639536,-0.457506203155893,
4.46321101183598));
#32287=CARTESIAN_POINT('Ctrl Pts',(14.4860329801035,-0.622549707754089,
4.19054718257559));
#32288=CARTESIAN_POINT('Ctrl Pts',(14.5096470962533,-0.63839484111024,3.87221739454711));
#32289=CARTESIAN_POINT('Ctrl Pts',(14.5332612124032,-0.501244206711231,
3.58451159745434));
#32290=CARTESIAN_POINT('Ctrl Pts',(14.5568753285531,-0.243966908844842,
3.39638048838484));
#32291=CARTESIAN_POINT('Ctrl Pts',(14.5804894447029,0.0717787570654544,
3.35291099727801));
#32292=CARTESIAN_POINT('Ctrl Pts',(14.6041035608528,0.370322144162233,3.46452089026927));
#32293=CARTESIAN_POINT('Ctrl Pts',(14.6277176770027,0.580115251486915,3.70446207957941));
#32294=CARTESIAN_POINT('Ctrl Pts',(14.6513317931525,0.650879700384091,4.0152309888134));
#32295=CARTESIAN_POINT('Ctrl Pts',(14.6749459093024,0.565656298155129,4.32234968564526));
#32296=CARTESIAN_POINT('Ctrl Pts',(14.6985600254523,0.344869426209941,4.55221503612336));
#32297=CARTESIAN_POINT('Ctrl Pts',(14.7221741416021,0.041432195817608,4.64973820947522));
#32298=CARTESIAN_POINT('Ctrl Pts',(14.745788257752,-0.271934549361806,4.59154709694401));
#32299=CARTESIAN_POINT('Ctrl Pts',(14.7694023739019,-0.520130285395982,
4.39158760667368));
#32300=CARTESIAN_POINT('Ctrl Pts',(14.7930164900517,-0.64367318065081,4.09778141619902));
#32301=CARTESIAN_POINT('Ctrl Pts',(14.8166306062016,-0.612955311082805,
3.78054123783642));
#32302=CARTESIAN_POINT('Ctrl Pts',(14.8402447223515,-0.435338447621071,
3.51589585985611));
#32303=CARTESIAN_POINT('Ctrl Pts',(14.8638588385013,-0.153389665944836,
3.36726945127358));
#32304=CARTESIAN_POINT('Ctrl Pts',(14.8874729546512,0.165319955489652,3.37028123293502));
#32305=CARTESIAN_POINT('Ctrl Pts',(14.9110870708011,0.444409630539555,3.52420969451069));
#32306=CARTESIAN_POINT('Ctrl Pts',(14.9347011869509,0.616993161964042,3.79216419995926));
#32307=CARTESIAN_POINT('Ctrl Pts',(14.9583153031008,0.641710593195818,4.10992889087348));
#32308=CARTESIAN_POINT('Ctrl Pts',(14.9819294192507,0.512636325700993,4.40134645341462));
#32309=CARTESIAN_POINT('Ctrl Pts',(15.0055435354005,0.260708010403211,4.59658262768273));
#32310=CARTESIAN_POINT('Ctrl Pts',(15.0291576515504,-0.0537065278721878,
4.64883488988255));
#32311=CARTESIAN_POINT('Ctrl Pts',(15.0527717677003,-0.355236031271534,
4.54560815721762));
#32312=CARTESIAN_POINT('Ctrl Pts',(15.0763858838501,-0.571652475026301,
4.31158258982903));
#32313=CARTESIAN_POINT('Ctrl Pts',(15.09212862795,-0.624530364890795,4.10584538053252));
#32314=CARTESIAN_POINT('Ctrl Pts',(15.1,-0.624993681275899,4.00281040303152));
#32315=CARTESIAN_POINT('Ctrl Pts',(15.1,-0.624993681275899,4.00281040303152));
#32316=CARTESIAN_POINT('Ctrl Pts',(15.1,-0.617358358083874,4.02914127082806));
#32317=CARTESIAN_POINT('Ctrl Pts',(15.1,-0.607931963506944,4.05484759228836));
#32318=CARTESIAN_POINT('Ctrl Pts',(15.1,-0.596773861259576,4.07974656001827));
#32319=CARTESIAN_POINT('Ctrl Pts',(15.1,-0.585871522029423,4.10407480030985));
#32320=CARTESIAN_POINT('Ctrl Pts',(15.1,-0.573314772633929,4.12763281365198));
#32321=CARTESIAN_POINT('Ctrl Pts',(15.1,-0.559143639302279,4.1502040881484));
#32322=CARTESIAN_POINT('Ctrl Pts',(15.1,-0.549626121151564,4.16536325076984));
#32323=CARTESIAN_POINT('Ctrl Pts',(15.1,-0.539380106047495,4.18007635520315));
#32324=CARTESIAN_POINT('Ctrl Pts',(15.1,-0.528417753985571,4.19426420824267));
#32325=CARTESIAN_POINT('Ctrl Pts',(15.1,-0.523814643226911,4.2002217124899));
#32326=CARTESIAN_POINT('Ctrl Pts',(15.1,-0.519084627089791,4.20608691507751));
#32327=CARTESIAN_POINT('Ctrl Pts',(15.1,-0.514239086396905,4.21184190560023));
#32328=CARTESIAN_POINT('Ctrl Pts',(15.1,-0.50085552272952,4.2277374035328));
#32329=CARTESIAN_POINT('Ctrl Pts',(15.1,-0.486572803760524,4.24281789068328));
#32330=CARTESIAN_POINT('Ctrl Pts',(15.1,-0.4714177983537,4.25697008589974));
#32331=CARTESIAN_POINT('Ctrl Pts',(15.1,-0.457151696655403,4.27029219637033));
#32332=CARTESIAN_POINT('Ctrl Pts',(15.1,-0.442112042545397,4.28279146400573));
#32333=CARTESIAN_POINT('Ctrl Pts',(15.1,-0.426369607892924,4.29437520287289));
#32334=CARTESIAN_POINT('Ctrl Pts',(15.1,-0.419074661497203,4.29974303548351));
#32335=CARTESIAN_POINT('Ctrl Pts',(15.1,-0.411628924918527,4.30491398987477));
#32336=CARTESIAN_POINT('Ctrl Pts',(15.1,-0.404040271526401,4.30987739070861));
#32337=CARTESIAN_POINT('Ctrl Pts',(15.1,-0.398073367501634,4.31378007737535));
#32338=CARTESIAN_POINT('Ctrl Pts',(15.1,-0.392026704362881,4.31754881952869));
#32339=CARTESIAN_POINT('Ctrl Pts',(15.1,-0.385904261325812,4.32117966642505));
#32340=CARTESIAN_POINT('Ctrl Pts',(15.1,-0.366868686798561,4.33246850264191));
#32341=CARTESIAN_POINT('Ctrl Pts',(15.1,-0.347097727375919,4.34242824684389));
#32342=CARTESIAN_POINT('Ctrl Pts',(15.1,-0.326713262272485,4.3509180109496));
#32343=CARTESIAN_POINT('Ctrl Pts',(15.1,-0.308010762698638,4.35870726657947));
#32344=CARTESIAN_POINT('Ctrl Pts',(15.1,-0.288791261952878,4.36525839133365));
#32345=CARTESIAN_POINT('Ctrl Pts',(15.1,-0.269173508333929,4.37043259773196));
#32346=CARTESIAN_POINT('Ctrl Pts',(12.5,-0.186196943290592,3.58169363627332));
#32347=CARTESIAN_POINT('Ctrl Pts',(12.5,-0.170588484282379,3.56594316788148));
#32348=CARTESIAN_POINT('Ctrl Pts',(12.5,-0.153797667832464,3.55144458439849));
#32349=CARTESIAN_POINT('Ctrl Pts',(12.5,-0.136060690067392,3.53823162417247));
#32350=CARTESIAN_POINT('Ctrl Pts',(12.5,-0.117990710310259,3.5247705978929));
#32351=CARTESIAN_POINT('Ctrl Pts',(12.5,-0.0989385549429972,3.51264262455394));
#32352=CARTESIAN_POINT('Ctrl Pts',(12.5,-0.0790990435859813,3.5018744512649));
#32353=CARTESIAN_POINT('Ctrl Pts',(12.5,-0.0668145727052721,3.49520688224936));
#32354=CARTESIAN_POINT('Ctrl Pts',(12.5,-0.054227138249592,3.4890605701039));
#32355=CARTESIAN_POINT('Ctrl Pts',(12.5,-0.0413735013057162,3.4834433907237));
#32356=CARTESIAN_POINT('Ctrl Pts',(12.5,-0.0353493612034326,3.48081077586818));
#32357=CARTESIAN_POINT('Ctrl Pts',(12.5,-0.0292710672153644,3.47829647656688));
#32358=CARTESIAN_POINT('Ctrl Pts',(12.5,-0.0231507758853709,3.47590397706369));
#32359=CARTESIAN_POINT('Ctrl Pts',(12.5,-0.00211397253512804,3.467680423829));
#32360=CARTESIAN_POINT('Ctrl Pts',(12.5,0.0194422610390746,3.46088402724794));
#32361=CARTESIAN_POINT('Ctrl Pts',(12.5,0.0413436963816045,3.45552737346533));
#32362=CARTESIAN_POINT('Ctrl Pts',(12.5,0.0650920698750741,3.44971899548849));
#32363=CARTESIAN_POINT('Ctrl Pts',(12.5,0.089246474293393,3.44560199012534));
#32364=CARTESIAN_POINT('Ctrl Pts',(12.5,0.113633446029948,3.44311473184586));
#32365=CARTESIAN_POINT('Ctrl Pts',(12.5,0.123118497624279,3.44214733936417));
#32366=CARTESIAN_POINT('Ctrl Pts',(12.5,0.132642564327611,3.44142688205345));
#32367=CARTESIAN_POINT('Ctrl Pts',(12.5,0.142169452875131,3.44095138714122));
#32368=CARTESIAN_POINT('Ctrl Pts',(12.5,0.170359862108328,3.43954438042575));
#32369=CARTESIAN_POINT('Ctrl Pts',(12.5,0.19861482332424,3.44027367679077));
#32370=CARTESIAN_POINT('Ctrl Pts',(12.5,0.226679319731597,3.44302987267532));
#32371=CARTESIAN_POINT('Ctrl Pts',(12.5,0.254743816138955,3.44578606855986));
#32372=CARTESIAN_POINT('Ctrl Pts',(12.5,0.282619254593541,3.45056842907764));
#32373=CARTESIAN_POINT('Ctrl Pts',(12.5,0.310093463203745,3.45730861053194));
#32374=CARTESIAN_POINT('Ctrl Pts',(15.0699957084852,-1.05870731373636E-5,
4.45788944868556));
#32375=CARTESIAN_POINT('Ctrl Pts',(15.0634386537186,0.0628625045491076,
4.45782850550181));
#32376=CARTESIAN_POINT('Ctrl Pts',(15.0568815989521,0.125761012144406,4.44477074790967));
#32377=CARTESIAN_POINT('Ctrl Pts',(15.0503245441856,0.183365120595825,4.41959809737683));
#32378=CARTESIAN_POINT('Ctrl Pts',(15.0424531721356,0.252515583017112,4.38937975928409));
#32379=CARTESIAN_POINT('Ctrl Pts',(15.0345818000857,0.314036477612831,4.34170308552782));
#32380=CARTESIAN_POINT('Ctrl Pts',(15.0267104280357,0.360556892971808,4.28228266426341));
#32381=CARTESIAN_POINT('Ctrl Pts',(15.0188390559858,0.407077308330786,4.222862242999));
#32382=CARTESIAN_POINT('Ctrl Pts',(15.0109676839358,0.438597244453022,4.15169807422645));
#32383=CARTESIAN_POINT('Ctrl Pts',(15.0030963118859,0.45133921416074,4.07731692107955));
#32384=CARTESIAN_POINT('Ctrl Pts',(14.9952249398359,0.464081183868457,4.00293576793266));
#32385=CARTESIAN_POINT('Ctrl Pts',(14.9873535677859,0.458045187161657,3.92533763041141));
#32386=CARTESIAN_POINT('Ctrl Pts',(14.979482195736,0.433954739621328,3.85382131653551));
#32387=CARTESIAN_POINT('Ctrl Pts',(14.971610823686,0.409864292080999,3.78230500265962));
#32388=CARTESIAN_POINT('Ctrl Pts',(14.9637394516361,0.367719393707138,3.71687051242907));
#32389=CARTESIAN_POINT('Ctrl Pts',(14.9558680795861,0.312570095196614,3.66535860215541));
#32390=CARTESIAN_POINT('Ctrl Pts',(14.9479967075362,0.257420796686091,3.61384669188175));
#32391=CARTESIAN_POINT('Ctrl Pts',(14.9401253354862,0.189267098038905,3.57625736156498));
#32392=CARTESIAN_POINT('Ctrl Pts',(14.9322539634362,0.116275803938161,3.55709495786573));
#32393=CARTESIAN_POINT('Ctrl Pts',(14.9243825913863,0.0432845098374172,
3.53793255416647));
#32394=CARTESIAN_POINT('Ctrl Pts',(14.9165112193363,-0.0345443797168851,
3.53719707708475));
#32395=CARTESIAN_POINT('Ctrl Pts',(14.9086398472864,-0.107884770736704,
3.55497662303181));
#32396=CARTESIAN_POINT('Ctrl Pts',(14.9007684752364,-0.181225161756525,
3.57275616897888));
#32397=CARTESIAN_POINT('Ctrl Pts',(14.8928971031865,-0.250077054241862,
3.60905073795473));
#32398=CARTESIAN_POINT('Ctrl Pts',(14.8850257311365,-0.306190019513209,
3.65951122309406));
#32399=CARTESIAN_POINT('Ctrl Pts',(14.8771543590866,-0.362302984784554,
3.70997170823338));
#32400=CARTESIAN_POINT('Ctrl Pts',(14.8692829870366,-0.405677022841909,
3.77459810953617));
#32401=CARTESIAN_POINT('Ctrl Pts',(14.8614116149867,-0.431114693744839,
3.84564633596564));
#32402=CARTESIAN_POINT('Ctrl Pts',(14.8535402429367,-0.45655236464777,3.91669456239511));
#32403=CARTESIAN_POINT('Ctrl Pts',(14.8456688708867,-0.464053668396277,
3.99416461395126));
#32404=CARTESIAN_POINT('Ctrl Pts',(14.8377974988368,-0.452719732759917,
4.06877337558629));
#32405=CARTESIAN_POINT('Ctrl Pts',(14.8299261267868,-0.441385797123556,
4.14338213722132));
#32406=CARTESIAN_POINT('Ctrl Pts',(14.8220547547369,-0.411216622102327,
4.21512960893523));
#32407=CARTESIAN_POINT('Ctrl Pts',(14.8141833826869,-0.365827335221939,
4.27541839855419));
#32408=CARTESIAN_POINT('Ctrl Pts',(14.806312010637,-0.32043804834155,4.33570718817315));
#32409=CARTESIAN_POINT('Ctrl Pts',(14.798440638587,-0.259828649602004,4.38453729569717));
#32410=CARTESIAN_POINT('Ctrl Pts',(14.7905692665371,-0.191261870645823,
4.41605748429924));
#32411=CARTESIAN_POINT('Ctrl Pts',(14.7837114138531,-0.131523763221734,
4.44351912740692));
#32412=CARTESIAN_POINT('Ctrl Pts',(14.7768535611691,-0.065745536276614,
4.45784152413683));
#32413=CARTESIAN_POINT('Ctrl Pts',(14.7699957084852,8.6346448269735E-6,
4.45789857801605));
#32414=CARTESIAN_POINT('Ctrl Pts',(12.5,0.310062960217722,4.54266560670548));
#32415=CARTESIAN_POINT('Ctrl Pts',(12.50787137205,0.220600394030941,4.59378185169648));
#32416=CARTESIAN_POINT('Ctrl Pts',(12.5236141161499,0.0159878432799406,
4.65085692712531));
#32417=CARTESIAN_POINT('Ctrl Pts',(12.5472282322997,-0.294892507759568,
4.580447501361));
#32418=CARTESIAN_POINT('Ctrl Pts',(12.5708423484496,-0.535054221536356,
4.37092866956447));
#32419=CARTESIAN_POINT('Ctrl Pts',(12.5944564645995,-0.647009713430093,
4.07251155115386));
#32420=CARTESIAN_POINT('Ctrl Pts',(12.6180705807493,-0.603894380709874,
3.75671714932517));
#32421=CARTESIAN_POINT('Ctrl Pts',(12.6416846968992,-0.416056506175611,
3.49922677321964));
#32422=CARTESIAN_POINT('Ctrl Pts',(12.6652988130491,-0.128505496873939,
3.36175035317655));
#32423=CARTESIAN_POINT('Ctrl Pts',(12.6889129291989,0.189841674427298,3.37723482234205));
#32424=CARTESIAN_POINT('Ctrl Pts',(12.7125270453488,0.462692468193658,3.54196933898577));
#32425=CARTESIAN_POINT('Ctrl Pts',(12.7361411614987,0.624655556881011,3.81647407445394));
#32426=CARTESIAN_POINT('Ctrl Pts',(12.7597552776485,0.636915702199809,4.13496208375113));
#32427=CARTESIAN_POINT('Ctrl Pts',(12.7833693937984,0.496534514683115,4.42110548633398));
#32428=CARTESIAN_POINT('Ctrl Pts',(12.8069835099483,0.237155397994168,4.60632802944461));
#32429=CARTESIAN_POINT('Ctrl Pts',(12.8305976260981,-0.0790596718614395,
4.64623983861064));
#32430=CARTESIAN_POINT('Ctrl Pts',(12.854211742248,-0.376327535803878,4.5312757721487));
#32431=CARTESIAN_POINT('Ctrl Pts',(12.8778258583979,-0.583405888470749,
4.28898776831928));
#32432=CARTESIAN_POINT('Ctrl Pts',(12.9014399745477,-0.650666957548692,
3.97744183415536));
#32433=CARTESIAN_POINT('Ctrl Pts',(12.9250540906976,-0.561991161265395,
3.67130212143154));
#32434=CARTESIAN_POINT('Ctrl Pts',(12.9486682068475,-0.338630270727757,
3.44393714350224));
#32435=CARTESIAN_POINT('Ctrl Pts',(12.9722823229973,-0.0341142786054444,
3.34983650006563));
#32436=CARTESIAN_POINT('Ctrl Pts',(12.9958964391472,0.278577437919422,3.41155206540036));
#32437=CARTESIAN_POINT('Ctrl Pts',(13.0195105552971,0.524506132150044,3.61429327464512));
#32438=CARTESIAN_POINT('Ctrl Pts',(13.0431246714469,0.644733280558021,3.90947178565704));
#32439=CARTESIAN_POINT('Ctrl Pts',(13.0667387875968,0.61044561006836,4.22634601343335));
#32440=CARTESIAN_POINT('Ctrl Pts',(13.0903529037467,0.429860399609997,4.4889748434194));
#32441=CARTESIAN_POINT('Ctrl Pts',(13.1139670198965,0.146256151980267,4.63441744826062));
#32442=CARTESIAN_POINT('Ctrl Pts',(13.1375811360464,-0.172399400609521,
4.62781749523177));
#32443=CARTESIAN_POINT('Ctrl Pts',(13.1611952521963,-0.449738236712957,
4.47075670902068));
#32444=CARTESIAN_POINT('Ctrl Pts',(13.1848093683461,-0.619294173608025,
4.2008758003961));
#32445=CARTESIAN_POINT('Ctrl Pts',(13.208423484496,-0.64043195068177,3.88285360784221));
#32446=CARTESIAN_POINT('Ctrl Pts',(13.2320376006459,-0.508085752511173,
3.59290636366459));
#32447=CARTESIAN_POINT('Ctrl Pts',(13.2556517167957,-0.253973266794505,
3.40052194335125));
#32448=CARTESIAN_POINT('Ctrl Pts',(13.2792658329456,0.0610056803032868,
3.3518066124833));
#32449=CARTESIAN_POINT('Ctrl Pts',(13.3028799490955,0.361364191435218,3.45843533922715));
#32450=CARTESIAN_POINT('Ctrl Pts',(13.3264940652453,0.575119258511334,3.69485380694));
#32451=CARTESIAN_POINT('Ctrl Pts',(13.3501081813952,0.65104299168552,4.00440268404554));
#32452=CARTESIAN_POINT('Ctrl Pts',(13.3737222975451,0.570939739771795,4.31289642727099));
#32453=CARTESIAN_POINT('Ctrl Pts',(13.3973364136949,0.354006804717113,4.54640236352309));
#32454=CARTESIAN_POINT('Ctrl Pts',(13.4209505298448,0.0522336745508671,
4.6489591696652));
#32455=CARTESIAN_POINT('Ctrl Pts',(13.4445646459947,-0.26205761933777,4.59598839317277));
#32456=CARTESIAN_POINT('Ctrl Pts',(13.4681787621445,-0.513544980480383,
4.40018484937968));
#32457=CARTESIAN_POINT('Ctrl Pts',(13.4917928782944,-0.64195771209056,4.10847422061066));
#32458=CARTESIAN_POINT('Ctrl Pts',(13.5154069944443,-0.616520809113462,
3.79076698974655));
#32459=CARTESIAN_POINT('Ctrl Pts',(13.5390211105941,-0.443330402422436,
3.52320390633144));
#32460=CARTESIAN_POINT('Ctrl Pts',(13.562635226744,-0.163892778617988,3.36990832590288));
#32461=CARTESIAN_POINT('Ctrl Pts',(13.5862493428939,0.154822890495328,3.36761860145296));
#32462=CARTESIAN_POINT('Ctrl Pts',(13.6098634590437,0.43643417612693,3.51688348138565));
#32463=CARTESIAN_POINT('Ctrl Pts',(13.6334775751936,0.613450973283793,3.78193059814177));
#32464=CARTESIAN_POINT('Ctrl Pts',(13.6570916913435,0.643449974253473,4.09923956510808));
#32465=CARTESIAN_POINT('Ctrl Pts',(13.6807058074933,0.519241709620395,4.39276507945606));
#32466=CARTESIAN_POINT('Ctrl Pts',(13.7043199236432,0.270593554659618,4.59216170834183));
#32467=CARTESIAN_POINT('Ctrl Pts',(13.7279340397931,-0.0429042293685969,
4.64964266158552));
#32468=CARTESIAN_POINT('Ctrl Pts',(13.7515481559429,-0.346119716157775,
4.55143222859795));
#32469=CARTESIAN_POINT('Ctrl Pts',(13.7751622720928,-0.566385203513325,
4.32106722332061));
#32470=CARTESIAN_POINT('Ctrl Pts',(13.7987763882427,-0.650912534047929,
4.01375622291695));
#32471=CARTESIAN_POINT('Ctrl Pts',(13.8223905043925,-0.57944414457563,3.70314844792952));
#32472=CARTESIAN_POINT('Ctrl Pts',(13.8460046205424,-0.369107932149097,
3.46368321387984));
#32473=CARTESIAN_POINT('Ctrl Pts',(13.8696187366923,-0.0703124342978696,
3.35275003110641));
#32474=CARTESIAN_POINT('Ctrl Pts',(13.8932328528421,0.245333927901481,3.3969348091043));
#32475=CARTESIAN_POINT('Ctrl Pts',(13.916846968992,0.502184306426786,3.58564835824111));
#32476=CARTESIAN_POINT('Ctrl Pts',(13.9404610851419,0.638682720042094,3.87366416276737));
#32477=CARTESIAN_POINT('Ctrl Pts',(13.9640752012917,0.62211637371287,4.19195723015293));
#32478=CARTESIAN_POINT('Ctrl Pts',(13.9876893174416,0.456455507660852,4.46424641105313));
#32479=CARTESIAN_POINT('Ctrl Pts',(14.0113034335915,0.181401901656729,4.62527570776815));
#32480=CARTESIAN_POINT('Ctrl Pts',(14.0349175497413,-0.137125932879425,
4.63645332836083));
#32481=CARTESIAN_POINT('Ctrl Pts',(14.0585316658912,-0.422790583021024,
4.49510047824495));
#32482=CARTESIAN_POINT('Ctrl Pts',(14.0821457820411,-0.60713052675338,4.23509335195577));
#32483=CARTESIAN_POINT('Ctrl Pts',(14.1057598981909,-0.645967413308333,
3.91874446730605));
#32484=CARTESIAN_POINT('Ctrl Pts',(14.1293740143408,-0.529993712466286,
3.62186903671368));
#32485=CARTESIAN_POINT('Ctrl Pts',(14.1529881304907,-0.287003328966194,
3.41561532377041));
#32486=CARTESIAN_POINT('Ctrl Pts',(14.1766022466405,0.0247694002478971,
3.34941346658496));
#32487=CARTESIAN_POINT('Ctrl Pts',(14.2002163627904,0.330605970264406,3.43912920108534));
#32488=CARTESIAN_POINT('Ctrl Pts',(14.2238304789403,0.557210518047066,3.66326152695696));
#32489=CARTESIAN_POINT('Ctrl Pts',(14.2474445950901,0.650275686248857,3.96809557204375));
#32490=CARTESIAN_POINT('Ctrl Pts',(14.27105871124,0.587497759452106,4.28057573538778));
#32491=CARTESIAN_POINT('Ctrl Pts',(14.2946728273899,0.383921904832036,4.52581397056352));
#32492=CARTESIAN_POINT('Ctrl Pts',(14.3182869435397,0.088336493108731,4.64503722732482));
#32493=CARTESIAN_POINT('Ctrl Pts',(14.3419010596896,-0.22841937412829,4.6096728222354));
#32494=CARTESIAN_POINT('Ctrl Pts',(14.3655151758395,-0.490432948250941,
4.42819608115853));
#32495=CARTESIAN_POINT('Ctrl Pts',(14.3891292919893,-0.634910852255616,
4.14409916841427));
#32496=CARTESIAN_POINT('Ctrl Pts',(14.4127434081392,-0.627227950688033,
3.82546788683648));
#32497=CARTESIAN_POINT('Ctrl Pts',(14.4363575242891,-0.469225504392149,
3.54866444115539));
#32498=CARTESIAN_POINT('Ctrl Pts',(14.4599716404389,-0.198769899531221,
3.38002670405092));
#32499=CARTESIAN_POINT('Ctrl Pts',(14.4835857565888,0.11932229545683,3.35996988316441));
#32500=CARTESIAN_POINT('Ctrl Pts',(14.5071998727387,0.408818071695872,3.49330073524378));
#32501=CARTESIAN_POINT('Ctrl Pts',(14.5308139888885,0.600337751131954,3.74806559342675));
#32502=CARTESIAN_POINT('Ctrl Pts',(14.5544281050384,0.647982309355475,4.06320828594604));
#32503=CARTESIAN_POINT('Ctrl Pts',(14.5780422211883,0.540333396317157,4.36320267272319));
#32504=CARTESIAN_POINT('Ctrl Pts',(14.6016563373381,0.303189823409542,4.57615301060753));
#32505=CARTESIAN_POINT('Ctrl Pts',(14.625270453488,-0.00661530128860875,
4.65102426869959));
#32506=CARTESIAN_POINT('Ctrl Pts',(14.6488845696379,-0.314835022974042,
4.56987302880665));
#32507=CARTESIAN_POINT('Ctrl Pts',(14.6724986857877,-0.547602339746838,
4.35214775046202));
#32508=CARTESIAN_POINT('Ctrl Pts',(14.6961128019376,-0.649132943719538,
4.05002781234082));
#32509=CARTESIAN_POINT('Ctrl Pts',(14.7197269180875,-0.595094318970103,
3.73591836064326));
#32510=CARTESIAN_POINT('Ctrl Pts',(14.7433410342373,-0.398437197867616,
3.48509791236843));
#32511=CARTESIAN_POINT('Ctrl Pts',(14.7669551503872,-0.1062918289807,3.35767733339665));
#32512=CARTESIAN_POINT('Ctrl Pts',(14.7905692665371,0.211327117384507,3.38419385377023));
#32513=CARTESIAN_POINT('Ctrl Pts',(14.8141833826869,0.478300047385911,3.5582926020622));
#32514=CARTESIAN_POINT('Ctrl Pts',(14.8377974988368,0.630645044771057,3.83824960712979));
#32515=CARTESIAN_POINT('Ctrl Pts',(14.8614116149867,0.631851559871185,4.15697121131127));
#32516=CARTESIAN_POINT('Ctrl Pts',(14.8850257311365,0.481630465478622,4.4380735902585));
#32517=CARTESIAN_POINT('Ctrl Pts',(14.9086398472864,0.215983244330552,4.61418854455152));
#32518=CARTESIAN_POINT('Ctrl Pts',(14.9322539634363,-0.101425794369151,
4.64310902247508));
#32519=CARTESIAN_POINT('Ctrl Pts',(14.9558680795861,-0.394527586443172,
4.517903766532));
#32520=CARTESIAN_POINT('Ctrl Pts',(14.979482195736,-0.593077772790822,4.26857965265179));
#32521=CARTESIAN_POINT('Ctrl Pts',(15.0030963118859,-0.649493436571599,
3.95488773069898));
#32522=CARTESIAN_POINT('Ctrl Pts',(15.0267104280357,-0.550252000240565,
3.65200904506483));
#32523=CARTESIAN_POINT('Ctrl Pts',(15.0503245441856,-0.319142060764588,
3.43252503194012));
#32524=CARTESIAN_POINT('Ctrl Pts',(15.0739386603355,-0.0115409051696555,
3.34904846156061));
#32525=CARTESIAN_POINT('Ctrl Pts',(15.0975527764853,0.298810377697559,3.42155963907315));
#32526=CARTESIAN_POINT('Ctrl Pts',(15.1211668926352,0.537575400322941,3.63273573589665));
#32527=CARTESIAN_POINT('Ctrl Pts',(15.1369096367351,0.610790903144771,3.83214323401692));
#32528=CARTESIAN_POINT('Ctrl Pts',(15.1447810087851,0.621570310124627,3.93461384266089));
#32529=CARTESIAN_POINT('Ctrl Pts',(12.4850729970716,0.282426015030316,4.49429601229446));
#32530=CARTESIAN_POINT('Ctrl Pts',(12.4929443691216,0.200937545576316,4.54085609598193));
#32531=CARTESIAN_POINT('Ctrl Pts',(12.5086871132215,0.0145627935155885,
4.59284387968754));
#32532=CARTESIAN_POINT('Ctrl Pts',(12.5323012293714,-0.268607755567932,
4.52871028073968));
#32533=CARTESIAN_POINT('Ctrl Pts',(12.5559153455213,-0.487363055256749,
4.3378665608173));
#32534=CARTESIAN_POINT('Ctrl Pts',(12.5795294616711,-0.589339580973024,
4.06604835489435));
#32535=CARTESIAN_POINT('Ctrl Pts',(12.603143577821,-0.550067261575934,3.77840176074865));
#32536=CARTESIAN_POINT('Ctrl Pts',(12.6267576939709,-0.378972002925158,
3.54386236016666));
#32537=CARTESIAN_POINT('Ctrl Pts',(12.6503718101207,-0.117051373585908,
3.41863967169675));
#32538=CARTESIAN_POINT('Ctrl Pts',(12.6739859262706,0.172920453180012,3.43274395851062));
#32539=CARTESIAN_POINT('Ctrl Pts',(12.6976000424204,0.42145114619533,3.58279513857084));
#32540=CARTESIAN_POINT('Ctrl Pts',(12.7212141585703,0.568977924911017,3.83283235195095));
#32541=CARTESIAN_POINT('Ctrl Pts',(12.7448282747202,0.580145282610399,4.12293246335278));
#32542=CARTESIAN_POINT('Ctrl Pts',(12.76844239087,0.45227673827436,4.38357095065208));
#32543=CARTESIAN_POINT('Ctrl Pts',(12.7920565070199,0.216016946852954,4.55228399108678));
#32544=CARTESIAN_POINT('Ctrl Pts',(12.8156706231698,-0.0720128197761896,
4.58863832766248));
#32545=CARTESIAN_POINT('Ctrl Pts',(12.8392847393196,-0.34278420811256,4.48392139165784));
#32546=CARTESIAN_POINT('Ctrl Pts',(12.8628988554695,-0.531404976945056,
4.26322932523642));
#32547=CARTESIAN_POINT('Ctrl Pts',(12.8865129716194,-0.592670842732518,
3.97945251867098));
#32548=CARTESIAN_POINT('Ctrl Pts',(12.9101270877692,-0.51189901575794,3.70060005900794));
#32549=CARTESIAN_POINT('Ctrl Pts',(12.9337412039191,-0.308447025930223,
3.49350087944474));
#32550=CARTESIAN_POINT('Ctrl Pts',(12.957355320069,-0.0310735592390789,
3.40778774002645));
#32551=CARTESIAN_POINT('Ctrl Pts',(12.9809694362188,0.253746902286204,3.46400239130434));
#32552=CARTESIAN_POINT('Ctrl Pts',(13.0045835523687,0.477755152237737,3.64867260076509));
#32553=CARTESIAN_POINT('Ctrl Pts',(13.0281976685186,0.587266054150949,3.91754086716214));
#32554=CARTESIAN_POINT('Ctrl Pts',(13.0518117846685,0.556034558024266,4.20617103876933));
#32555=CARTESIAN_POINT('Ctrl Pts',(13.0754259008183,0.391545509324759,4.44539088570928));
#32556=CARTESIAN_POINT('Ctrl Pts',(13.0990400169682,0.133219853633759,4.57786970637232));
#32557=CARTESIAN_POINT('Ctrl Pts',(13.122654133118,-0.157032867368526,4.57185802915678));
#32558=CARTESIAN_POINT('Ctrl Pts',(13.1462682492679,-0.409651568547275,
4.42879659435664));
#32559=CARTESIAN_POINT('Ctrl Pts',(13.1698823654178,-0.564094419600429,
4.1829710707208));
#32560=CARTESIAN_POINT('Ctrl Pts',(13.1934964815676,-0.583348116144335,
3.89329525626321));
#32561=CARTESIAN_POINT('Ctrl Pts',(13.2171105977175,-0.462798375770677,
3.62919197644995));
#32562=CARTESIAN_POINT('Ctrl Pts',(13.2407247138674,-0.231335782947555,
3.45395542080054));
#32563=CARTESIAN_POINT('Ctrl Pts',(13.2643388300172,0.055568040665587,3.40958224975729));
#32564=CARTESIAN_POINT('Ctrl Pts',(13.2879529461671,0.329154596505292,3.50670680265737));
#32565=CARTESIAN_POINT('Ctrl Pts',(13.311567062317,0.523856961936024,3.72205250428141));
#32566=CARTESIAN_POINT('Ctrl Pts',(13.3351811784668,0.593013359693284,4.00401025814095));
#32567=CARTESIAN_POINT('Ctrl Pts',(13.3587952946167,0.520049977633468,4.28500692572024));
#32568=CARTESIAN_POINT('Ctrl Pts',(13.3824094107666,0.322452998189994,4.49769969952106));
#32569=CARTESIAN_POINT('Ctrl Pts',(13.4060235269164,0.0475779130258999,
4.59111527567571));
#32570=CARTESIAN_POINT('Ctrl Pts',(13.4296376430663,-0.238699550200797,
4.5428659610613));
#32571=CARTESIAN_POINT('Ctrl Pts',(13.4532517592162,-0.467771004553565,
4.36451503980497));
#32572=CARTESIAN_POINT('Ctrl Pts',(13.476865875366,-0.584737881352888,4.09880555174689));
#32573=CARTESIAN_POINT('Ctrl Pts',(13.5004799915159,-0.561568254327815,
3.80941662539381));
#32574=CARTESIAN_POINT('Ctrl Pts',(13.5240941076658,-0.403814885886516,
3.56570233148043));
#32575=CARTESIAN_POINT('Ctrl Pts',(13.5477082238157,-0.149284468950505,
3.42607049712074));
#32576=CARTESIAN_POINT('Ctrl Pts',(13.5713223399655,0.141023010189178,3.42398486344345));
#32577=CARTESIAN_POINT('Ctrl Pts',(13.5949364561154,0.39753334322815,3.55994526707815));
#32578=CARTESIAN_POINT('Ctrl Pts',(13.6185505722652,0.55877204319843,3.8013678508274));
#32579=CARTESIAN_POINT('Ctrl Pts',(13.6421646884151,0.586097133215014,4.09039401187145));
#32580=CARTESIAN_POINT('Ctrl Pts',(13.665778804565,0.47295996523623,4.35775661870721));
#32581=CARTESIAN_POINT('Ctrl Pts',(13.6893929207148,0.24647464915429,4.53938036140496));
#32582=CARTESIAN_POINT('Ctrl Pts',(13.7130070368647,-0.0390800323908759,
4.59173784568287));
#32583=CARTESIAN_POINT('Ctrl Pts',(13.7366211530146,-0.315268912124245,
4.50228123595558));
#32584=CARTESIAN_POINT('Ctrl Pts',(13.7602352691644,-0.515901402373503,
4.29244943148197));
#32585=CARTESIAN_POINT('Ctrl Pts',(13.7838493853143,-0.59289453017979,4.01253008491428));
#32586=CARTESIAN_POINT('Ctrl Pts',(13.8074635014642,-0.527796356489121,
3.72960781627073));
#32587=CARTESIAN_POINT('Ctrl Pts',(13.831077617614,-0.336208111796874,3.51148691674935));
#32588=CARTESIAN_POINT('Ctrl Pts',(13.8546917337639,-0.0640452526541193,
3.4104415783338));
#32589=CARTESIAN_POINT('Ctrl Pts',(13.8783058499138,0.223466497127862,3.45068801978614));
#32590=CARTESIAN_POINT('Ctrl Pts',(13.9019199660636,0.457422945247278,3.62258090124322));
#32591=CARTESIAN_POINT('Ctrl Pts',(13.9255340822135,0.581754800262342,3.88492489705937));
#32592=CARTESIAN_POINT('Ctrl Pts',(13.9491481983634,0.566665067602596,4.17484744237197));
#32593=CARTESIAN_POINT('Ctrl Pts',(13.9727623145132,0.415770106744681,4.42286658094793));
#32594=CARTESIAN_POINT('Ctrl Pts',(13.9963764306631,0.165232945489059,4.56954279968241));
#32595=CARTESIAN_POINT('Ctrl Pts',(14.019990546813,-0.124903441395439,4.57972412169294));
#32596=CARTESIAN_POINT('Ctrl Pts',(14.0436046629628,-0.385105849054417,
4.45097052228405));
#32597=CARTESIAN_POINT('Ctrl Pts',(14.0672187791127,-0.553014959135429,
4.21413869785145));
#32598=CARTESIAN_POINT('Ctrl Pts',(14.0908328952626,-0.58839018453545,3.92598704378684));
#32599=CARTESIAN_POINT('Ctrl Pts',(14.1144470114124,-0.482753606228458,
3.65557310990793));
#32600=CARTESIAN_POINT('Ctrl Pts',(14.1380611275623,-0.261421765577673,
3.46770347791168));
#32601=CARTESIAN_POINT('Ctrl Pts',(14.1616752437122,0.0225616210391343,
3.40740241293002));
#32602=CARTESIAN_POINT('Ctrl Pts',(14.185289359862,0.301137958114838,3.48912148496193));
#32603=CARTESIAN_POINT('Ctrl Pts',(14.2089034760119,0.507544487205137,3.69327614952086));
#32604=CARTESIAN_POINT('Ctrl Pts',(14.2325175921618,0.592314446747875,3.97093932005559));
#32605=CARTESIAN_POINT('Ctrl Pts',(14.2561317083116,0.535132125826274,4.25556708484021));
#32606=CARTESIAN_POINT('Ctrl Pts',(14.2797458244615,0.349701665714674,4.47894641865396));
#32607=CARTESIAN_POINT('Ctrl Pts',(14.3033599406114,0.0804627670229728,
4.58754290912926));
#32608=CARTESIAN_POINT('Ctrl Pts',(14.3269740567612,-0.208059593914322,
4.55533065134682));
#32609=CARTESIAN_POINT('Ctrl Pts',(14.3505881729111,-0.44671902479684,4.39002953712461));
#32610=CARTESIAN_POINT('Ctrl Pts',(14.374202289061,-0.578319131624566,4.13125512920294));
#32611=CARTESIAN_POINT('Ctrl Pts',(14.3978164052108,-0.571321032683373,
3.84102451585645));
#32612=CARTESIAN_POINT('Ctrl Pts',(14.4214305213607,-0.427401871100662,
3.58889348396707));
#32613=CARTESIAN_POINT('Ctrl Pts',(14.4450446375106,-0.181052875819672,
3.43528699049651));
#32614=CARTESIAN_POINT('Ctrl Pts',(14.4686587536604,0.108686701521778,3.41701790091169));
#32615=CARTESIAN_POINT('Ctrl Pts',(14.4922728698103,0.372378754238714,3.53846452970905));
#32616=CARTESIAN_POINT('Ctrl Pts',(14.5158869859602,0.546827646247725,3.77052134686598));
#32617=CARTESIAN_POINT('Ctrl Pts',(14.53950110211,0.59022548618159,4.05757432072539));
#32618=CARTESIAN_POINT('Ctrl Pts',(14.5631152182599,0.492171679592087,4.3308292078278));
#32619=CARTESIAN_POINT('Ctrl Pts',(14.5867293344098,0.276165503816305,4.52479857226205));
#32620=CARTESIAN_POINT('Ctrl Pts',(14.6103434505596,-0.00602565743375084,
4.59299630554951));
#32621=CARTESIAN_POINT('Ctrl Pts',(14.6339575667095,-0.286772727926288,
4.51907834617235));
#32622=CARTESIAN_POINT('Ctrl Pts',(14.6575716828594,-0.49879271786407,4.32075964763751));
#32623=CARTESIAN_POINT('Ctrl Pts',(14.6811857990092,-0.591273560669336,
4.04556866666751));
#32624=CARTESIAN_POINT('Ctrl Pts',(14.7047999151591,-0.542051578672567,
3.75945683743125));
#32625=CARTESIAN_POINT('Ctrl Pts',(14.728414031309,-0.362923162297683,3.53099285177933));
#32626=CARTESIAN_POINT('Ctrl Pts',(14.7520281474588,-0.0968176839575538,
3.41492969374656));
#32627=CARTESIAN_POINT('Ctrl Pts',(14.7756422636087,0.192490826988301,3.43908270827084));
#32628=CARTESIAN_POINT('Ctrl Pts',(14.7992563797586,0.435667569828913,3.59766345479839));
#32629=CARTESIAN_POINT('Ctrl Pts',(14.8228704959084,0.574433549780463,3.85266695881428));
#32630=CARTESIAN_POINT('Ctrl Pts',(14.8464846120583,0.575532524168,4.14297984400973));
#32631=CARTESIAN_POINT('Ctrl Pts',(14.8700987282082,0.438701136655627,4.39902663091346));
#32632=CARTESIAN_POINT('Ctrl Pts',(14.893712844358,0.196731937819222,4.55944387228049));
#32633=CARTESIAN_POINT('Ctrl Pts',(14.9173269605079,-0.0923853752310475,
4.58578657160514));
#32634=CARTESIAN_POINT('Ctrl Pts',(14.9409410766578,-0.359362027571537,
4.47174127747511));
#32635=CARTESIAN_POINT('Ctrl Pts',(14.9645551928076,-0.540214773976066,
4.24464025294543));
#32636=CARTESIAN_POINT('Ctrl Pts',(14.9881693089575,-0.59160192159185,3.95890873763601));
#32637=CARTESIAN_POINT('Ctrl Pts',(15.0117834251074,-0.501206205285789,
3.68302663884805));
#32638=CARTESIAN_POINT('Ctrl Pts',(15.0353975412572,-0.290695865081771,
3.48310596742652));
#32639=CARTESIAN_POINT('Ctrl Pts',(15.0590116574071,-0.0105122258222001,
3.40706994202017));
#32640=CARTESIAN_POINT('Ctrl Pts',(15.082625773557,0.272176412698783,3.47311795657709));
#32641=CARTESIAN_POINT('Ctrl Pts',(15.1062398897068,0.489659512974156,3.66547122397039));
#32642=CARTESIAN_POINT('Ctrl Pts',(15.1219826338067,0.5563490739778,3.84710486709154));
#32643=CARTESIAN_POINT('Ctrl Pts',(15.1298540058567,0.566167676482186,3.94044192881839));
#32644=CARTESIAN_POINT('Ctrl Pts',(12.4701459941433,0.254789069842909,4.44592641788345));
#32645=CARTESIAN_POINT('Ctrl Pts',(12.4780173661933,0.181274697121691,4.48793034026739));
#32646=CARTESIAN_POINT('Ctrl Pts',(12.4937601102932,0.0131377437512366,
4.53483083224977));
#32647=CARTESIAN_POINT('Ctrl Pts',(12.517374226443,-0.242323003376296,4.47697306011837));
#32648=CARTESIAN_POINT('Ctrl Pts',(12.5409883425929,-0.439671888977142,
4.30480445207012));
#32649=CARTESIAN_POINT('Ctrl Pts',(12.5646024587428,-0.531669448515955,
4.05958515863483));
#32650=CARTESIAN_POINT('Ctrl Pts',(12.5882165748926,-0.496240142441994,
3.80008637217214));
#32651=CARTESIAN_POINT('Ctrl Pts',(12.6118306910425,-0.341887499674706,
3.58849794711368));
#32652=CARTESIAN_POINT('Ctrl Pts',(12.6354448071924,-0.105597250297878,
3.47552899021694));
#32653=CARTESIAN_POINT('Ctrl Pts',(12.6590589233422,0.155999231932725,3.4882530946792));
#32654=CARTESIAN_POINT('Ctrl Pts',(12.6826730394921,0.380209824197002,3.62362093815591));
#32655=CARTESIAN_POINT('Ctrl Pts',(12.706287155642,0.513300292941022,3.84919062944795));
#32656=CARTESIAN_POINT('Ctrl Pts',(12.7299012717918,0.52337486302099,4.11090284295443));
#32657=CARTESIAN_POINT('Ctrl Pts',(12.7535153879417,0.408018961865605,4.34603641497018));
#32658=CARTESIAN_POINT('Ctrl Pts',(12.7771295040916,0.194878495711741,4.49823995272895));
#32659=CARTESIAN_POINT('Ctrl Pts',(12.8007436202414,-0.0649659676909401,
4.53103681671432));
#32660=CARTESIAN_POINT('Ctrl Pts',(12.8243577363913,-0.30924088042124,4.43656701116699));
#32661=CARTESIAN_POINT('Ctrl Pts',(12.8479718525412,-0.479404065419363,
4.23747088215356));
#32662=CARTESIAN_POINT('Ctrl Pts',(12.871585968691,-0.534674727916345,3.9814632031866));
#32663=CARTESIAN_POINT('Ctrl Pts',(12.8952000848409,-0.461806870250484,
3.72989799658434));
#32664=CARTESIAN_POINT('Ctrl Pts',(12.9188142009908,-0.278263781132688,
3.54306461538724));
#32665=CARTESIAN_POINT('Ctrl Pts',(12.9424283171406,-0.0280328398727138,
3.46573897998727));
#32666=CARTESIAN_POINT('Ctrl Pts',(12.9660424332905,0.228916366652986,3.51645271720832));
#32667=CARTESIAN_POINT('Ctrl Pts',(12.9896565494404,0.431004172325429,3.68305192688505));
#32668=CARTESIAN_POINT('Ctrl Pts',(13.0132706655902,0.529798827743877,3.92560994866724));
#32669=CARTESIAN_POINT('Ctrl Pts',(13.0368847817401,0.501623505980173,4.1859960641053));
#32670=CARTESIAN_POINT('Ctrl Pts',(13.06049889789,0.353230619039521,4.40180692799916));
#32671=CARTESIAN_POINT('Ctrl Pts',(13.0841130140398,0.120183555287252,4.52132196448402));
#32672=CARTESIAN_POINT('Ctrl Pts',(13.1077271301897,-0.14166633412753,4.51589856308179));
#32673=CARTESIAN_POINT('Ctrl Pts',(13.1313412463396,-0.369564900381594,
4.38683647969259));
#32674=CARTESIAN_POINT('Ctrl Pts',(13.1549553624894,-0.508894665592834,
4.16506634104549));
#32675=CARTESIAN_POINT('Ctrl Pts',(13.1785694786393,-0.5262642816069,3.9037369046842));
#32676=CARTESIAN_POINT('Ctrl Pts',(13.2021835947892,-0.417510999030181,
3.66547758923531));
#32677=CARTESIAN_POINT('Ctrl Pts',(13.225797710939,-0.208698299100604,3.50738889824983));
#32678=CARTESIAN_POINT('Ctrl Pts',(13.2494118270889,0.0501304010278875,
3.46735788703128));
#32679=CARTESIAN_POINT('Ctrl Pts',(13.2730259432388,0.296945001575366,3.55497826608759));
#32680=CARTESIAN_POINT('Ctrl Pts',(13.2966400593886,0.472594665360713,3.74925120162283));
#32681=CARTESIAN_POINT('Ctrl Pts',(13.3202541755385,0.534983727701048,4.00361783223636));
#32682=CARTESIAN_POINT('Ctrl Pts',(13.3438682916884,0.469160215495142,4.25711742416948));
#32683=CARTESIAN_POINT('Ctrl Pts',(13.3674824078382,0.290899191662876,4.44899703551904));
#32684=CARTESIAN_POINT('Ctrl Pts',(13.3910965239881,0.0429221515009326,
4.53327138168622));
#32685=CARTESIAN_POINT('Ctrl Pts',(13.414710640138,-0.215341481063824,4.48974352894983));
#32686=CARTESIAN_POINT('Ctrl Pts',(13.4383247562878,-0.421997028626747,
4.32884523023027));
#32687=CARTESIAN_POINT('Ctrl Pts',(13.4619388724377,-0.527518050615216,
4.08913688288313));
#32688=CARTESIAN_POINT('Ctrl Pts',(13.4855529885876,-0.506615699542168,
3.82806626104107));
#32689=CARTESIAN_POINT('Ctrl Pts',(13.5091671047374,-0.364299369350597,
3.60820075662942));
#32690=CARTESIAN_POINT('Ctrl Pts',(13.5327812208873,-0.134676159283021,
3.48223266833859));
#32691=CARTESIAN_POINT('Ctrl Pts',(13.5563953370372,0.127223129883027,3.48035112543394));
#32692=CARTESIAN_POINT('Ctrl Pts',(13.580009453187,0.35863251032937,3.60300705277064));
#32693=CARTESIAN_POINT('Ctrl Pts',(13.6036235693369,0.504093113113068,3.82080510351303));
#32694=CARTESIAN_POINT('Ctrl Pts',(13.6272376854868,0.528744292176554,4.08154845863482));
#32695=CARTESIAN_POINT('Ctrl Pts',(13.6508518016366,0.426678220852065,4.32274815795836));
#32696=CARTESIAN_POINT('Ctrl Pts',(13.6744659177865,0.222355743648963,4.48659901446809));
#32697=CARTESIAN_POINT('Ctrl Pts',(13.6980800339364,-0.0352558354131549,
4.53383302978021));
#32698=CARTESIAN_POINT('Ctrl Pts',(13.7216941500862,-0.284418108090716,
4.45313024331322));
#32699=CARTESIAN_POINT('Ctrl Pts',(13.7453082662361,-0.465417601233682,
4.26383163964332));
#32700=CARTESIAN_POINT('Ctrl Pts',(13.768922382386,-0.534876526311652,4.01130394691162));
#32701=CARTESIAN_POINT('Ctrl Pts',(13.7925364985358,-0.476148568402614,
3.75606718461195));
#32702=CARTESIAN_POINT('Ctrl Pts',(13.8161506146857,-0.303308291444651,
3.55929061961886));
#32703=CARTESIAN_POINT('Ctrl Pts',(13.8397647308356,-0.0577780710103693,
3.46813312556118));
#32704=CARTESIAN_POINT('Ctrl Pts',(13.8633788469854,0.201599066354243,3.50444123046797));
#32705=CARTESIAN_POINT('Ctrl Pts',(13.8869929631353,0.412661584067771,3.65951344424533));
#32706=CARTESIAN_POINT('Ctrl Pts',(13.9106070792852,0.52482688048259,3.89618563135138));
#32707=CARTESIAN_POINT('Ctrl Pts',(13.934221195435,0.511213761492322,4.157737654591));
#32708=CARTESIAN_POINT('Ctrl Pts',(13.9578353115849,0.375084705828511,4.38148675084272));
#32709=CARTESIAN_POINT('Ctrl Pts',(13.9814494277348,0.149063989321389,4.51380989159668));
#32710=CARTESIAN_POINT('Ctrl Pts',(14.0050635438846,-0.112680949911453,
4.52299491502504));
#32711=CARTESIAN_POINT('Ctrl Pts',(14.0286776600345,-0.347421115087809,
4.40684056632315));
#32712=CARTESIAN_POINT('Ctrl Pts',(14.0522917761844,-0.498899391517477,
4.19318404374712));
#32713=CARTESIAN_POINT('Ctrl Pts',(14.0759058923342,-0.530812955762567,
3.93322962026762));
#32714=CARTESIAN_POINT('Ctrl Pts',(14.0995200084841,-0.435513499990629,
3.68927718310219));
#32715=CARTESIAN_POINT('Ctrl Pts',(14.123134124634,-0.235840202189154,3.51979163205294));
#32716=CARTESIAN_POINT('Ctrl Pts',(14.1467482407838,0.020353841830372,3.46539135927508));
#32717=CARTESIAN_POINT('Ctrl Pts',(14.1703623569337,0.271669945965271,3.53911376883853));
#32718=CARTESIAN_POINT('Ctrl Pts',(14.1939764730836,0.457878456363209,3.72329077208477));
#32719=CARTESIAN_POINT('Ctrl Pts',(14.2175905892334,0.534353207246894,3.97378306806742));
#32720=CARTESIAN_POINT('Ctrl Pts',(14.2412047053833,0.482766492200443,4.23055843429265));
#32721=CARTESIAN_POINT('Ctrl Pts',(14.2648188215332,0.315481426597312,4.4320788667444));
#32722=CARTESIAN_POINT('Ctrl Pts',(14.288432937683,0.0725890409372144,4.53004859093371));
#32723=CARTESIAN_POINT('Ctrl Pts',(14.3120470538329,-0.187699813700353,
4.50098848045824));
#32724=CARTESIAN_POINT('Ctrl Pts',(14.3356611699828,-0.40300510134274,4.35186299309067));
#32725=CARTESIAN_POINT('Ctrl Pts',(14.3592752861326,-0.521727410993515,
4.11841108999162));
#32726=CARTESIAN_POINT('Ctrl Pts',(14.3828894022825,-0.515414114678713,
3.85658114487643));
#32727=CARTESIAN_POINT('Ctrl Pts',(14.4065035184324,-0.385578237809175,
3.62912252677875));
#32728=CARTESIAN_POINT('Ctrl Pts',(14.4301176345822,-0.163335852108122,
3.49054727694211));
#32729=CARTESIAN_POINT('Ctrl Pts',(14.4537317507321,0.0980511075867261,
3.47406591865897));
#32730=CARTESIAN_POINT('Ctrl Pts',(14.477345866882,0.335939436781555,3.58362832417432));
#32731=CARTESIAN_POINT('Ctrl Pts',(14.5009599830318,0.493317541363497,3.79297710030521));
#32732=CARTESIAN_POINT('Ctrl Pts',(14.5245740991817,0.532468663007706,4.05194035550473));
#32733=CARTESIAN_POINT('Ctrl Pts',(14.5481882153316,0.444009962867018,4.2984557429324));
#32734=CARTESIAN_POINT('Ctrl Pts',(14.5718023314814,0.249141184223067,4.47344413391656));
#32735=CARTESIAN_POINT('Ctrl Pts',(14.5954164476313,-0.00543601357889273,
4.53496834239941));
#32736=CARTESIAN_POINT('Ctrl Pts',(14.6190305637812,-0.258710432878536,
4.46828366353805));
#32737=CARTESIAN_POINT('Ctrl Pts',(14.642644679931,-0.449983095981302,4.28937154481299));
#32738=CARTESIAN_POINT('Ctrl Pts',(14.6662587960809,-0.533414177619135,
4.0411095209942));
#32739=CARTESIAN_POINT('Ctrl Pts',(14.6898729122308,-0.489008838375032,
3.78299531421925));
#32740=CARTESIAN_POINT('Ctrl Pts',(14.7134870283806,-0.327409126727749,
3.57688779119022));
#32741=CARTESIAN_POINT('Ctrl Pts',(14.7371011445305,-0.0873435389344073,
3.47218205409647));
#32742=CARTESIAN_POINT('Ctrl Pts',(14.7607152606804,0.173654536592096,3.49397156277145));
#32743=CARTESIAN_POINT('Ctrl Pts',(14.7843293768302,0.393035092271916,3.63703430753458));
#32744=CARTESIAN_POINT('Ctrl Pts',(14.8079434929801,0.518222054789869,3.86708431049878));
#32745=CARTESIAN_POINT('Ctrl Pts',(14.8315576091299,0.519213488464815,4.12898847670818));
#32746=CARTESIAN_POINT('Ctrl Pts',(14.8551717252798,0.395771807832633,4.35997967156842));
#32747=CARTESIAN_POINT('Ctrl Pts',(14.8787858414297,0.177480631307892,4.50469920000947));
#32748=CARTESIAN_POINT('Ctrl Pts',(14.9023999575796,-0.0833449560929437,
4.52846412073519));
#32749=CARTESIAN_POINT('Ctrl Pts',(14.9260140737294,-0.324196468699902,
4.42557878841823));
#32750=CARTESIAN_POINT('Ctrl Pts',(14.9496281898793,-0.487351775161311,
4.22070085323907));
#32751=CARTESIAN_POINT('Ctrl Pts',(14.9732423060292,-0.533710406612102,
3.96292974457304));
#32752=CARTESIAN_POINT('Ctrl Pts',(14.996856422179,-0.452160410331013,3.71404423263127));
#32753=CARTESIAN_POINT('Ctrl Pts',(15.0204705383289,-0.262249669398955,
3.53368690291293));
#32754=CARTESIAN_POINT('Ctrl Pts',(15.0440846544788,-0.0094835464747447,
3.46509142247974));
#32755=CARTESIAN_POINT('Ctrl Pts',(15.0676987706286,0.245542447700007,3.52467627408104));
#32756=CARTESIAN_POINT('Ctrl Pts',(15.0913128867785,0.441743625625371,3.69820671204414));
#32757=CARTESIAN_POINT('Ctrl Pts',(15.1070556308784,0.501907244810829,3.86206650016617));
#32758=CARTESIAN_POINT('Ctrl Pts',(15.1149270029284,0.510765042839744,3.94627001497588));
#32759=CARTESIAN_POINT('Ctrl Pts',(12.4552189912149,0.227152124655503,4.39755682347243));
#32760=CARTESIAN_POINT('Ctrl Pts',(12.4630903632649,0.161611848667067,4.43500458455284));
#32761=CARTESIAN_POINT('Ctrl Pts',(12.4788331073648,0.0117126939868845,
4.476817784812));
#32762=CARTESIAN_POINT('Ctrl Pts',(12.5024472235147,-0.216038251184659,
4.42523583949706));
#32763=CARTESIAN_POINT('Ctrl Pts',(12.5260613396645,-0.391980722697534,
4.27174234332294));
#32764=CARTESIAN_POINT('Ctrl Pts',(12.5496754558144,-0.473999316058885,
4.05312196237532));
#32765=CARTESIAN_POINT('Ctrl Pts',(12.5732895719643,-0.442413023308054,
3.82177098359562));
#32766=CARTESIAN_POINT('Ctrl Pts',(12.5969036881141,-0.304802996424253,
3.6331335340607));
#32767=CARTESIAN_POINT('Ctrl Pts',(12.620517804264,-0.0941431270098475,
3.53241830873714));
#32768=CARTESIAN_POINT('Ctrl Pts',(12.6441319204139,0.139078010685439,3.54376223084778));
#32769=CARTESIAN_POINT('Ctrl Pts',(12.6677460365637,0.338968502198674,3.66444673774097));
#32770=CARTESIAN_POINT('Ctrl Pts',(12.6913601527136,0.457622660971028,3.86554890694496));
#32771=CARTESIAN_POINT('Ctrl Pts',(12.7149742688635,0.46660444343158,4.09887322255608));
#32772=CARTESIAN_POINT('Ctrl Pts',(12.7385883850133,0.36376118545685,4.30850187928827));
#32773=CARTESIAN_POINT('Ctrl Pts',(12.7622025011632,0.173740044570527,4.44419591437112));
#32774=CARTESIAN_POINT('Ctrl Pts',(12.7858166173131,-0.0579191156056905,
4.47343530576616));
#32775=CARTESIAN_POINT('Ctrl Pts',(12.809430733463,-0.275697552729921,4.38921263067613));
#32776=CARTESIAN_POINT('Ctrl Pts',(12.8330448496128,-0.42740315389367,4.2117124390707));
#32777=CARTESIAN_POINT('Ctrl Pts',(12.8566589657627,-0.476678613100171,
3.98347388770222));
#32778=CARTESIAN_POINT('Ctrl Pts',(12.8802730819125,-0.411714724743029,
3.75919593416074));
#32779=CARTESIAN_POINT('Ctrl Pts',(12.9038871980624,-0.248080536335154,
3.59262835132974));
#32780=CARTESIAN_POINT('Ctrl Pts',(12.9275013142123,-0.0249921205063485,
3.52369021994808));
#32781=CARTESIAN_POINT('Ctrl Pts',(12.9511154303621,0.204085831019768,3.5689030431123));
#32782=CARTESIAN_POINT('Ctrl Pts',(12.974729546512,0.384253192413122,3.71743125300502));
#32783=CARTESIAN_POINT('Ctrl Pts',(12.9983436626619,0.472331601336806,3.93367903017235));
#32784=CARTESIAN_POINT('Ctrl Pts',(13.0219577788117,0.44721245393608,4.16582108944128));
#32785=CARTESIAN_POINT('Ctrl Pts',(13.0455718949616,0.314915728754283,4.35822297028905));
#32786=CARTESIAN_POINT('Ctrl Pts',(13.0691860111115,0.107147256940744,4.46477422259573));
#32787=CARTESIAN_POINT('Ctrl Pts',(13.0928001272613,-0.126299800886535,
4.4599390970068));
#32788=CARTESIAN_POINT('Ctrl Pts',(13.1164142434112,-0.329478232215912,
4.34487636502855));
#32789=CARTESIAN_POINT('Ctrl Pts',(13.1400283595611,-0.453694911585238,
4.14716161137019));
#32790=CARTESIAN_POINT('Ctrl Pts',(13.1636424757109,-0.469180447069464,
3.9141785531052));
#32791=CARTESIAN_POINT('Ctrl Pts',(13.1872565918608,-0.372223622289685,
3.70176320202068));
#32792=CARTESIAN_POINT('Ctrl Pts',(13.2108707080107,-0.186060815253654,
3.56082237569912));
#32793=CARTESIAN_POINT('Ctrl Pts',(13.2344848241605,0.0446927613901878,
3.52513352430527));
#32794=CARTESIAN_POINT('Ctrl Pts',(13.2580989403104,0.26473540664544,3.60324972951781));
#32795=CARTESIAN_POINT('Ctrl Pts',(13.2817130564603,0.421332368785403,3.77644989896424));
#32796=CARTESIAN_POINT('Ctrl Pts',(13.3053271726101,0.476954095708811,4.00322540633176));
#32797=CARTESIAN_POINT('Ctrl Pts',(13.32894128876,0.418270453356816,4.22922792261873));
#32798=CARTESIAN_POINT('Ctrl Pts',(13.3525554049099,0.259345385135757,4.40029437151701));
#32799=CARTESIAN_POINT('Ctrl Pts',(13.3761695210597,0.0382663899759653,
4.47542748769673));
#32800=CARTESIAN_POINT('Ctrl Pts',(13.3997836372096,-0.19198341192685,4.43662109683837));
#32801=CARTESIAN_POINT('Ctrl Pts',(13.4233977533595,-0.376223052699929,
4.29317542065556));
#32802=CARTESIAN_POINT('Ctrl Pts',(13.4470118695093,-0.470298219877544,
4.07946821401937));
#32803=CARTESIAN_POINT('Ctrl Pts',(13.4706259856592,-0.451663144756522,
3.84671589668833));
#32804=CARTESIAN_POINT('Ctrl Pts',(13.4942401018091,-0.324783852814677,
3.65069918177841));
#32805=CARTESIAN_POINT('Ctrl Pts',(13.5178542179589,-0.120067849615538,
3.53839483955645));
#32806=CARTESIAN_POINT('Ctrl Pts',(13.5414683341088,0.113423249576877,3.53671738742444));
#32807=CARTESIAN_POINT('Ctrl Pts',(13.5650824502587,0.319731677430589,3.64606883846313));
#32808=CARTESIAN_POINT('Ctrl Pts',(13.5886965664085,0.449414183027706,3.84024235619866));
#32809=CARTESIAN_POINT('Ctrl Pts',(13.6123106825584,0.471391451138094,4.07270290539818));
#32810=CARTESIAN_POINT('Ctrl Pts',(13.6359247987083,0.380396476467901,4.28773969720951));
#32811=CARTESIAN_POINT('Ctrl Pts',(13.6595389148581,0.198236838143636,4.43381766753122));
#32812=CARTESIAN_POINT('Ctrl Pts',(13.683153031008,-0.0314316384354341,
4.47592821387755));
#32813=CARTESIAN_POINT('Ctrl Pts',(13.7067671471579,-0.253567304057185,
4.40397925067086));
#32814=CARTESIAN_POINT('Ctrl Pts',(13.7303812633077,-0.414933800093862,
4.23521384780468));
#32815=CARTESIAN_POINT('Ctrl Pts',(13.7539953794576,-0.476858522443512,
4.01007780890896));
#32816=CARTESIAN_POINT('Ctrl Pts',(13.7776094956075,-0.424500780316106,
3.78252655295316));
#32817=CARTESIAN_POINT('Ctrl Pts',(13.8012236117573,-0.270408471092428,
3.60709432248837));
#32818=CARTESIAN_POINT('Ctrl Pts',(13.8248377279072,-0.0515108893666192,
3.52582467278856));
#32819=CARTESIAN_POINT('Ctrl Pts',(13.8484518440571,0.179731635580624,3.55819444114981));
#32820=CARTESIAN_POINT('Ctrl Pts',(13.8720659602069,0.367900222888263,3.69644598724744));
#32821=CARTESIAN_POINT('Ctrl Pts',(13.8956800763568,0.467898960702838,3.90744636564338));
#32822=CARTESIAN_POINT('Ctrl Pts',(13.9192941925067,0.455762455382048,4.14062786681004));
#32823=CARTESIAN_POINT('Ctrl Pts',(13.9429083086565,0.33439930491234,4.34010692073752));
#32824=CARTESIAN_POINT('Ctrl Pts',(13.9665224248064,0.132895033153719,4.45807698351094));
#32825=CARTESIAN_POINT('Ctrl Pts',(13.9901365409563,-0.100458458427467,
4.46626570835715));
#32826=CARTESIAN_POINT('Ctrl Pts',(14.0137506571061,-0.309736381121202,
4.36271061036225));
#32827=CARTESIAN_POINT('Ctrl Pts',(14.037364773256,-0.444783823899526,4.1722293896428));
#32828=CARTESIAN_POINT('Ctrl Pts',(14.0609788894059,-0.473235726989685,
3.94047219674841));
#32829=CARTESIAN_POINT('Ctrl Pts',(14.0845930055557,-0.388273393752801,
3.72298125629644));
#32830=CARTESIAN_POINT('Ctrl Pts',(14.1082071217056,-0.210258638800633,
3.5718797861942));
#32831=CARTESIAN_POINT('Ctrl Pts',(14.1318212378555,0.0181460626216094,
3.52338030562014));
#32832=CARTESIAN_POINT('Ctrl Pts',(14.1554353540053,0.242201933815703,3.58910605271512));
#32833=CARTESIAN_POINT('Ctrl Pts',(14.1790494701552,0.40821242552128,3.75330539464867));
#32834=CARTESIAN_POINT('Ctrl Pts',(14.2026635863051,0.476391967745912,3.97662681607925));
#32835=CARTESIAN_POINT('Ctrl Pts',(14.2262777024549,0.430400858574612,4.20554978374509));
#32836=CARTESIAN_POINT('Ctrl Pts',(14.2498918186048,0.28126118747995,4.38521131483484));
#32837=CARTESIAN_POINT('Ctrl Pts',(14.2735059347547,0.0647153148514563,
4.47255427273816));
#32838=CARTESIAN_POINT('Ctrl Pts',(14.2971200509045,-0.167340033486385,
4.44664630956965));
#32839=CARTESIAN_POINT('Ctrl Pts',(14.3207341670544,-0.359291177888639,
4.31369644905674));
#32840=CARTESIAN_POINT('Ctrl Pts',(14.3443482832043,-0.465135690362464,
4.10556705078029));
#32841=CARTESIAN_POINT('Ctrl Pts',(14.3679623993541,-0.459507196674052,
3.87213777389641));
#32842=CARTESIAN_POINT('Ctrl Pts',(14.391576515504,-0.343754604517688,3.66935156959044));
#32843=CARTESIAN_POINT('Ctrl Pts',(14.4151906316539,-0.145618828396573,
3.5458075633877));
#32844=CARTESIAN_POINT('Ctrl Pts',(14.4388047478037,0.0874155136516737,
3.53111393640625));
#32845=CARTESIAN_POINT('Ctrl Pts',(14.4624188639536,0.299500119324396,3.6287921186396));
#32846=CARTESIAN_POINT('Ctrl Pts',(14.4860329801035,0.439807436479269,3.81543285374444));
#32847=CARTESIAN_POINT('Ctrl Pts',(14.5096470962533,0.474711839833821,4.04630639028407));
#32848=CARTESIAN_POINT('Ctrl Pts',(14.5332612124032,0.395848246141948,4.26608227803701));
#32849=CARTESIAN_POINT('Ctrl Pts',(14.5568753285531,0.22211686462983,4.42208969557108));
#32850=CARTESIAN_POINT('Ctrl Pts',(14.5804894447029,-0.00484636972403486,
4.47694037924932));
#32851=CARTESIAN_POINT('Ctrl Pts',(14.6041035608528,-0.230648137830783,
4.41748898090375));
#32852=CARTESIAN_POINT('Ctrl Pts',(14.6277176770027,-0.401173474098533,
4.25798344198848));
#32853=CARTESIAN_POINT('Ctrl Pts',(14.6513317931525,-0.475554794568933,
4.03665037532088));
#32854=CARTESIAN_POINT('Ctrl Pts',(14.6749459093024,-0.435966098077497,
3.80653379100725));
#32855=CARTESIAN_POINT('Ctrl Pts',(14.6985600254523,-0.291895091157815,
3.62278273060111));
#32856=CARTESIAN_POINT('Ctrl Pts',(14.7221741416021,-0.077869393911261,
3.52943441444639));
#32857=CARTESIAN_POINT('Ctrl Pts',(14.745788257752,0.15481824619589,3.54886041727207));
#32858=CARTESIAN_POINT('Ctrl Pts',(14.7694023739019,0.350402614714918,3.67640516027076));
#32859=CARTESIAN_POINT('Ctrl Pts',(14.7930164900517,0.462010559799276,3.88150166218328));
#32860=CARTESIAN_POINT('Ctrl Pts',(14.8166306062016,0.46289445276163,4.11499710940664));
#32861=CARTESIAN_POINT('Ctrl Pts',(14.8402447223515,0.352842479009638,4.32093271222338));
#32862=CARTESIAN_POINT('Ctrl Pts',(14.8638588385013,0.158229324796562,4.44995452773844));
#32863=CARTESIAN_POINT('Ctrl Pts',(14.8874729546512,-0.07430453695484,4.47114166986524));
#32864=CARTESIAN_POINT('Ctrl Pts',(14.9110870708011,-0.289030909828268,
4.37941629936134));
#32865=CARTESIAN_POINT('Ctrl Pts',(14.9347011869509,-0.434488776346555,
4.1967614535327));
#32866=CARTESIAN_POINT('Ctrl Pts',(14.9583153031008,-0.475818891632353,
3.96695075151007));
#32867=CARTESIAN_POINT('Ctrl Pts',(14.9819294192507,-0.403114615376237,
3.74506182641449));
#32868=CARTESIAN_POINT('Ctrl Pts',(15.0055435354005,-0.233803473716137,
3.58426783839933));
#32869=CARTESIAN_POINT('Ctrl Pts',(15.0291576515504,-0.00845486712728951,
3.5231129029393));
#32870=CARTESIAN_POINT('Ctrl Pts',(15.0527717677003,0.218908482701231,3.57623459158499));
#32871=CARTESIAN_POINT('Ctrl Pts',(15.0763858838501,0.393827738276586,3.73094220011788));
#32872=CARTESIAN_POINT('Ctrl Pts',(15.09212862795,0.447465415643859,3.87702813324079));
#32873=CARTESIAN_POINT('Ctrl Pts',(15.1,0.455362409197302,3.95209810113337));
#32874=CARTESIAN_POINT('',(15.1,0.455362409197302,3.95209810113338));
#32875=CARTESIAN_POINT('Ctrl Pts',(15.1,0.455362409197302,3.95209810113337));
#32876=CARTESIAN_POINT('Ctrl Pts',(15.1,0.461198486074795,3.93070554260298));
#32877=CARTESIAN_POINT('Ctrl Pts',(15.1,0.46535922191849,3.9089149747703));
#32878=CARTESIAN_POINT('Ctrl Pts',(15.1,0.467933495509747,3.88694781877637));
#32879=CARTESIAN_POINT('Ctrl Pts',(15.1,0.470556099470815,3.86456824322593));
#32880=CARTESIAN_POINT('Ctrl Pts',(15.1,0.471533159003394,3.84200460508655));
#32881=CARTESIAN_POINT('Ctrl Pts',(15.1,0.470938919222204,3.8194389967166));
#32882=CARTESIAN_POINT('Ctrl Pts',(15.1,0.470570970565677,3.80546654730098));
#32883=CARTESIAN_POINT('Ctrl Pts',(15.1,0.469600118414825,3.7914923521806));
#32884=CARTESIAN_POINT('Ctrl Pts',(15.1,0.468037922355437,3.77755218535593));
#32885=CARTESIAN_POINT('Ctrl Pts',(15.1,0.467305764617198,3.77101881782393));
#32886=CARTESIAN_POINT('Ctrl Pts',(15.1,0.466444065557791,3.76449770946228));
#32887=CARTESIAN_POINT('Ctrl Pts',(15.1,0.465455885979624,3.7580011302485));
#32888=CARTESIAN_POINT('Ctrl Pts',(15.1,0.462059294618766,3.73567095330476));
#32889=CARTESIAN_POINT('Ctrl Pts',(15.1,0.45716703427379,3.71360451488159));
#32890=CARTESIAN_POINT('Ctrl Pts',(15.1,0.450855318277529,3.69195899424001));
#32891=CARTESIAN_POINT('Ctrl Pts',(15.1,0.444011336009419,3.66848810937402));
#32892=CARTESIAN_POINT('Ctrl Pts',(15.1,0.435499564516811,3.64551127788848));
#32893=CARTESIAN_POINT('Ctrl Pts',(15.1,0.425460105602329,3.62314791088594));
#32894=CARTESIAN_POINT('Ctrl Pts',(15.1,0.421555366121865,3.61444992000866));
#32895=CARTESIAN_POINT('Ctrl Pts',(15.1,0.417417266816347,3.60584160863805));
#32896=CARTESIAN_POINT('Ctrl Pts',(15.1,0.413065612826793,3.5973533346642));
#32897=CARTESIAN_POINT('Ctrl Pts',(15.1,0.400188909388694,3.57223622128044));
#32898=CARTESIAN_POINT('Ctrl Pts',(15.1,0.385429835973237,3.54813135585314));
#32899=CARTESIAN_POINT('Ctrl Pts',(15.1,0.369010648251791,3.52520488756047));
#32900=CARTESIAN_POINT('Ctrl Pts',(15.1,0.352591460530346,3.50227841926781));
#32901=CARTESIAN_POINT('Ctrl Pts',(15.1,0.334512091502091,3.48052876229398));
#32902=CARTESIAN_POINT('Ctrl Pts',(15.1,0.31493781544227,3.46010549098216));
#32903=CARTESIAN_POINT('Ctrl Pts',(14.8800042915148,-1.01702808208336E-5,
4.45785711824254));
#32904=CARTESIAN_POINT('Ctrl Pts',(14.8824938458936,-0.0238866377941533,
4.45787702641871));
#32905=CARTESIAN_POINT('Ctrl Pts',(14.8849834002724,-0.0477600743578134,
4.45604121816599));
#32906=CARTESIAN_POINT('Ctrl Pts',(14.8874729546512,-0.0713366221418418,
4.45232291776013));
#32907=CARTESIAN_POINT('Ctrl Pts',(14.8953443267012,-0.145879994579315,
4.44056654636394));
#32908=CARTESIAN_POINT('Ctrl Pts',(14.9032156987511,-0.217455452203791,
4.40999142286264));
#32909=CARTESIAN_POINT('Ctrl Pts',(14.9110870708011,-0.277486158769077,
4.36426138680722));
#32910=CARTESIAN_POINT('Ctrl Pts',(14.918958442851,-0.337516865334364,4.31853135075179));
#32911=CARTESIAN_POINT('Ctrl Pts',(14.926829814901,-0.38600282084046,4.25764640214225));
#32912=CARTESIAN_POINT('Ctrl Pts',(14.9347011869509,-0.417134151141141,
4.18890214416703));
#32913=CARTESIAN_POINT('Ctrl Pts',(14.9425725590009,-0.448265481441821,
4.12015788619182));
#32914=CARTESIAN_POINT('Ctrl Pts',(14.9504439310508,-0.462042186537087,
4.04355431885095));
#32915=CARTESIAN_POINT('Ctrl Pts',(14.9583153031008,-0.456813159708701,
3.96827104766458));
#32916=CARTESIAN_POINT('Ctrl Pts',(14.9661866751508,-0.451584132880315,
3.89298777647821));
#32917=CARTESIAN_POINT('Ctrl Pts',(14.9740580472007,-0.427349374128277,
3.81902480144635));
#32918=CARTESIAN_POINT('Ctrl Pts',(14.9819294192507,-0.387013471142241,
3.7552443159279));
#32919=CARTESIAN_POINT('Ctrl Pts',(14.9898007913006,-0.346677568156205,
3.69146383040944));
#32920=CARTESIAN_POINT('Ctrl Pts',(14.9976721633506,-0.290240520936171,
3.63786583440439));
#32921=CARTESIAN_POINT('Ctrl Pts',(15.0055435354005,-0.224463896228013,
3.60087434715852));
#32922=CARTESIAN_POINT('Ctrl Pts',(15.0134149074505,-0.158687271519854,
3.56388285991266));
#32923=CARTESIAN_POINT('Ctrl Pts',(15.0212862795004,-0.0835710693235713,
3.54349788142598));
#32924=CARTESIAN_POINT('Ctrl Pts',(15.0291576515504,-0.00811907658734153,
3.54215900695692));
#32925=CARTESIAN_POINT('Ctrl Pts',(15.0370290236004,0.067332916148885,3.54082013248786));
#32926=CARTESIAN_POINT('Ctrl Pts',(15.0449003956503,0.143120699425059,3.55852736203643));
#32927=CARTESIAN_POINT('Ctrl Pts',(15.0527717677003,0.210167800325704,3.59316557823286));
#32928=CARTESIAN_POINT('Ctrl Pts',(15.0606431397502,0.27721490122635,3.62780379442929));
#32929=CARTESIAN_POINT('Ctrl Pts',(15.0685145118002,0.335521319751467,3.67937299727358));
#32930=CARTESIAN_POINT('Ctrl Pts',(15.0763858838501,0.378083948355844,3.74167908197646));
#32931=CARTESIAN_POINT('Ctrl Pts',(15.0842572559001,0.420646576960222,3.80398516667934));
#32932=CARTESIAN_POINT('Ctrl Pts',(15.09212862795,0.447465415643859,3.87702813324079));
#32933=CARTESIAN_POINT('Ctrl Pts',(15.1,0.455362409197302,3.95209810113337));
#32934=CARTESIAN_POINT('Ctrl Pts',(12.5,0.310062960217722,4.54266560670548));
#32935=CARTESIAN_POINT('Ctrl Pts',(12.5,0.283442099593322,4.54921865641189));
#32936=CARTESIAN_POINT('Ctrl Pts',(12.5,0.256466577744696,4.55390832200786));
#32937=CARTESIAN_POINT('Ctrl Pts',(12.5,0.229324391633413,4.55669460918752));
#32938=CARTESIAN_POINT('Ctrl Pts',(12.5,0.202804350211112,4.55941702996513));
#32939=CARTESIAN_POINT('Ctrl Pts',(12.5,0.176124140498118,4.56032157710196));
#32940=CARTESIAN_POINT('Ctrl Pts',(12.5,0.149491279718871,4.55933465732487));
#32941=CARTESIAN_POINT('Ctrl Pts',(12.5,0.131604301980395,4.55867182909064));
#32942=CARTESIAN_POINT('Ctrl Pts',(12.5,0.113739373486447,4.5571550748263));
#32943=CARTESIAN_POINT('Ctrl Pts',(12.5,0.0959711573489174,4.5547553284502));
#32944=CARTESIAN_POINT('Ctrl Pts',(12.5,0.0885102514788159,4.55374767063663));
#32945=CARTESIAN_POINT('Ctrl Pts',(12.5,0.0810658284660142,4.55258395860043));
#32946=CARTESIAN_POINT('Ctrl Pts',(12.5,0.0736590895785168,4.55126509319275));
#32947=CARTESIAN_POINT('Ctrl Pts',(12.5,0.0532014046082737,4.54762233847462));
#32948=CARTESIAN_POINT('Ctrl Pts',(12.5,0.0329999615976937,4.54279338637244));
#32949=CARTESIAN_POINT('Ctrl Pts',(12.5,0.0131662989716721,4.53674486487483));
#32950=CARTESIAN_POINT('Ctrl Pts',(12.5,-0.00550403753485725,4.53105111411095));
#32951=CARTESIAN_POINT('Ctrl Pts',(12.5,-0.0238485481480196,4.52427602479051));
#32952=CARTESIAN_POINT('Ctrl Pts',(12.5,-0.0417515783368052,4.51643454453567));
#32953=CARTESIAN_POINT('Ctrl Pts',(12.5,-0.0500477299146631,4.51280085190917));
#32954=CARTESIAN_POINT('Ctrl Pts',(12.5,-0.058248775177811,4.50893813195896));
#32955=CARTESIAN_POINT('Ctrl Pts',(12.5,-0.0663415323109863,4.50484786558969));
#32956=CARTESIAN_POINT('Ctrl Pts',(12.5,-0.0727048112135971,4.50163171746301));
#32957=CARTESIAN_POINT('Ctrl Pts',(12.5,-0.0789919703630761,4.49827952355299));
#32958=CARTESIAN_POINT('Ctrl Pts',(12.5,-0.085197598682301,4.4947927546146));
#32959=CARTESIAN_POINT('Ctrl Pts',(12.5,-0.104491803581693,4.48395188067351));
#32960=CARTESIAN_POINT('Ctrl Pts',(12.5,-0.123002674071495,4.47180959856144));
#32961=CARTESIAN_POINT('Ctrl Pts',(12.5,-0.140547257611399,4.45840101528927));
#32962=CARTESIAN_POINT('Ctrl Pts',(12.5,-0.156644205929787,4.44609879839914));
#32963=CARTESIAN_POINT('Ctrl Pts',(12.5,-0.17192740174072,4.43272977950413));
#32964=CARTESIAN_POINT('Ctrl Pts',(12.5,-0.186217277007305,4.41832740439832));
#32965=CARTESIAN_POINT('Origin',(15.1,0.,4.));
#32966=CARTESIAN_POINT('',(15.1,-1.16619037896906,2.5));
#32967=CARTESIAN_POINT('',(15.1,1.16619037896906,2.5));
#32968=CARTESIAN_POINT('',(15.1,1.25,2.5));
#32969=CARTESIAN_POINT('Origin',(15.1,0.,4.));
#32970=CARTESIAN_POINT('Origin',(15.1,0.,4.));
#32971=CARTESIAN_POINT('',(15.1,2.75545529808154E-17,5.725));
#32972=CARTESIAN_POINT('Origin',(15.1,0.,5.5));
#32973=CARTESIAN_POINT('',(15.1,1.5,4.225));
#32974=CARTESIAN_POINT('Origin',(15.1,1.5,4.));
#32975=CARTESIAN_POINT('',(15.1,-1.5,4.225));
#32976=CARTESIAN_POINT('Origin',(15.1,-1.5,4.));
#32977=CARTESIAN_POINT('Origin',(14.4,-1.5,4.));
#32978=CARTESIAN_POINT('',(14.5,-1.5,4.225));
#32979=CARTESIAN_POINT('Origin',(14.5,-1.5,4.));
#32980=CARTESIAN_POINT('',(14.4,-1.5,4.225));
#32981=CARTESIAN_POINT('Origin',(14.4,1.5,4.));
#32982=CARTESIAN_POINT('',(14.5,1.5,4.225));
#32983=CARTESIAN_POINT('Origin',(14.5,1.5,4.));
#32984=CARTESIAN_POINT('',(14.4,1.5,4.225));
#32985=CARTESIAN_POINT('Origin',(14.4,0.,5.5));
#32986=CARTESIAN_POINT('',(14.5,-2.75545529808154E-17,5.725));
#32987=CARTESIAN_POINT('Origin',(14.5,0.,5.5));
#32988=CARTESIAN_POINT('',(14.4,-2.75545529808154E-17,5.725));
#32989=CARTESIAN_POINT('Origin',(14.4,2.5,2.5));
#32990=CARTESIAN_POINT('',(14.5,1.16619037896906,2.5));
#32991=CARTESIAN_POINT('',(14.5,-1.16619037896906,2.5));
#32992=CARTESIAN_POINT('',(14.5,1.25,2.5));
#32993=CARTESIAN_POINT('',(14.5,1.16619037896906,2.5));
#32994=CARTESIAN_POINT('',(14.5,-1.16619037896906,2.5));
#32995=CARTESIAN_POINT('Origin',(14.5,0.,4.));
#32996=CARTESIAN_POINT('Origin',(14.5,0.,4.));
#32997=CARTESIAN_POINT('',(14.5,-1.34711147906209E-16,5.1));
#32998=CARTESIAN_POINT('Origin',(14.5,0.,4.));
#32999=CARTESIAN_POINT('Origin',(14.5,0.,4.));
#33000=CARTESIAN_POINT('Origin',(12.5,0.,4.));
#33001=CARTESIAN_POINT('Origin',(12.5,0.,4.));
#33002=CARTESIAN_POINT('',(12.5,-1.34711147906209E-16,5.1));
#33003=CARTESIAN_POINT('',(12.5,-1.34711147906209E-16,5.1));
#33004=CARTESIAN_POINT('Origin',(12.5,0.,4.));
#33005=CARTESIAN_POINT('Origin',(12.5,0.,4.));
#43439=UNCERTAINTY_MEASURE_WITH_UNIT(LENGTH_MEASURE(0.001),#43522,
'DISTANCE_ACCURACY_VALUE',
'Maximum model space distance between geometric entities at asserted c
onnectivities');
#43453=UNCERTAINTY_MEASURE_WITH_UNIT(LENGTH_MEASURE(0.001),#43522,
'DISTANCE_ACCURACY_VALUE',
'Maximum model space distance between geometric entities at asserted c
onnectivities');
#43507=(
GEOMETRIC_REPRESENTATION_CONTEXT(3)
GLOBAL_UNCERTAINTY_ASSIGNED_CONTEXT((#43439))
GLOBAL_UNIT_ASSIGNED_CONTEXT((#43522,#43524,#43525))
REPRESENTATION_CONTEXT('','3D')
);
#43521=(
GEOMETRIC_REPRESENTATION_CONTEXT(3)
GLOBAL_UNCERTAINTY_ASSIGNED_CONTEXT((#43453))
GLOBAL_UNIT_ASSIGNED_CONTEXT((#43522,#43524,#43525))
REPRESENTATION_CONTEXT('','3D')
);
#43522=(
LENGTH_UNIT()
NAMED_UNIT(*)
SI_UNIT(.CENTI.,.METRE.)
);
#43524=(
NAMED_UNIT(*)
PLANE_ANGLE_UNIT()
SI_UNIT($,.RADIAN.)
);
#43525=(
NAMED_UNIT(*)
SI_UNIT($,.STERADIAN.)
SOLID_ANGLE_UNIT()
);
#43579=SHAPE_DEFINITION_REPRESENTATION(#43658,#43847);
#43658=PRODUCT_DEFINITION_SHAPE('',$,#43915);
#43847=SHAPE_REPRESENTATION('',(#20691),#43507);
#43861=PRODUCT_DEFINITION_CONTEXT('part definition',#44064,'design');
#43915=PRODUCT_DEFINITION('Flanged lead nut','Flanged lead nut',#43982,
#43861);
#43982=PRODUCT_DEFINITION_FORMATION('',$,#44119);
#44064=APPLICATION_CONTEXT(
'Core Data for Automotive Mechanical Design Process');
#44065=PRODUCT_CONTEXT('part definition',#44064,'mechanical');
#44119=PRODUCT('Flanged lead nut','Flanged lead nut','Flanged lead nut',
(#44065));
#44203=COLOUR_RGB('Black',0.12,0.14,0.17);
#44204=FILL_AREA_STYLE_COLOUR('',#44203);
#44205=FILL_AREA_STYLE('',(#44204));
#44206=SURFACE_STYLE_FILL_AREA(#44205);
#44207=SURFACE_SIDE_STYLE('',(#44206));
#44208=SURFACE_STYLE_USAGE(.BOTH.,#44207);
#44209=PRESENTATION_STYLE_ASSIGNMENT((#44208));
ENDSEC;
END-ISO-10303-21;
